ISO-10303-21;
HEADER;
FILE_DESCRIPTION (('STEP AP214'),
    '1' );
FILE_NAME ('Snap Open Cable Crossbars 15.step',
    '2026-10-08T22:59:04',
    ( '' ),
    ( '' ),
    'SwSTEP 2.0',
    'SolidWorks 2020',
    '' );
FILE_SCHEMA (( 'AUTOMOTIVE_DESIGN' ));
ENDSEC;

DATA;
#33=CARTESIAN_POINT ( 'NONE',  ( 18.39999999999999503, 64.52683809664910086, -56.87310748452440379 ) ) ;
#131=DIRECTION ( 'NONE',  ( -0.000000000000000000, -6.982962677686266711E-15, 1.000000000000000000 ) ) ;
#190=CARTESIAN_POINT ( 'NONE',  ( 18.39999999999999503, 70.35000000001159037, -56.87310748452436115 ) ) ;
#390=CARTESIAN_POINT ( 'NONE',  ( -18.41431012584568805, 64.51252797080333323, -45.24987147142272903 ) ) ;
#419=CARTESIAN_POINT ( 'NONE',  ( -18.40000000000000213, 64.52683809664901560, -45.34905355133235361 ) ) ;
#421=CARTESIAN_POINT ( 'NONE',  ( -12.25000000000000178, 66.15000000001155911, -52.77310748452439526 ) ) ;
#601=CARTESIAN_POINT ( 'NONE',  ( -16.87331047859649757, 66.05000000001153637, -48.67310748452439384 ) ) ;
#783=LINE ( 'NONE', #80319, #8482 ) ;
#989=CARTESIAN_POINT ( 'NONE',  ( -20.65000000000000568, 68.75000000001153921, -48.67310748452437252 ) ) ;
#1151=CARTESIAN_POINT ( 'NONE',  ( -16.83199318825828072, 66.06935387203033372, -48.79552229631519111 ) ) ;
#1286=VERTEX_POINT ( 'NONE', #149882 ) ;
#1308=ORIENTED_EDGE ( 'NONE', *, *, #192763, .F. ) ;
#1350=DIRECTION ( 'NONE',  ( 1.186688945009010077E-16, 1.000000000000000000, 6.982962677686266711E-15 ) ) ;
#1364=EDGE_CURVE ( 'NONE', #205644, #71110, #67688, .T. ) ;
#1563=CARTESIAN_POINT ( 'NONE',  ( -16.88705144915421030, 66.05000000001159322, -56.59212888981229383 ) ) ;
#1577=CARTESIAN_POINT ( 'NONE',  ( -17.11825945287482753, 66.05000000001157900, -56.77310748452439526 ) ) ;
#1595=EDGE_CURVE ( 'NONE', #206343, #132612, #121869, .T. ) ;
#1626=CARTESIAN_POINT ( 'NONE',  ( 20.99999999999999645, 66.25000000001162448, -60.27310748452439526 ) ) ;
#1746=CARTESIAN_POINT ( 'NONE',  ( -16.87683809663752399, 52.34166666667822199, -52.77310748452448763 ) ) ;
#1766=ADVANCED_FACE ( 'NONE', ( #197641 ), #77681, .F. ) ;
#1831=ORIENTED_EDGE ( 'NONE', *, *, #22736, .F. ) ;
#1863=EDGE_CURVE ( 'NONE', #84975, #128539, #78956, .T. ) ;
#2043=DIRECTION ( 'NONE',  ( 1.000000000000000000, -1.186688945009010077E-16, -8.286604613020808509E-31 ) ) ;
#2126=DIRECTION ( 'NONE',  ( 0.000000000000000000, 6.982962677686266711E-15, -1.000000000000000000 ) ) ;
#2351=VERTEX_POINT ( 'NONE', #66830 ) ;
#2425=AXIS2_PLACEMENT_3D ( 'NONE', #153513, #135160, #16531 ) ;
#2451=CARTESIAN_POINT ( 'NONE',  ( -16.92280123533709713, 66.05000000001153637, -48.87373979860947060 ) ) ;
#2512=CARTESIAN_POINT ( 'NONE',  ( -16.97683809663752186, 66.15000000001158753, -56.87310748452438958 ) ) ;
#2842=CARTESIAN_POINT ( 'NONE',  ( -16.92280123533699410, 66.05000000001157900, -56.67247517043902860 ) ) ;
#2956=( BOUNDED_CURVE ( )  B_SPLINE_CURVE ( 3, ( #125601, #225954, #47333, #82588 ),
 .UNSPECIFIED., .F., .F. ) 
 B_SPLINE_CURVE_WITH_KNOTS ( ( 4, 4 ),
 ( 2.589852378279005940, 2.850972632318389710 ),
 .UNSPECIFIED. ) 
 CURVE ( )  GEOMETRIC_REPRESENTATION_ITEM ( )  RATIONAL_B_SPLINE_CURVE ( ( 1.000000000000000000, 0.9943260843901262636, 0.9943260843901262636, 1.000000000000000000 ) ) 
 REPRESENTATION_ITEM ( '' )  );
#3088=ORIENTED_EDGE ( 'NONE', *, *, #13395, .T. ) ;
#3274=( BOUNDED_CURVE ( )  B_SPLINE_CURVE ( 3, ( #69912, #15062, #71190, #209393 ),
 .UNSPECIFIED., .F., .T. ) 
 B_SPLINE_CURVE_WITH_KNOTS ( ( 4, 4 ),
 ( 0.5235987755983128045, 1.570796326794896558 ),
 .UNSPECIFIED. ) 
 CURVE ( )  GEOMETRIC_REPRESENTATION_ITEM ( )  RATIONAL_B_SPLINE_CURVE ( ( 1.000000000000000000, 0.9106836025229614329, 0.9106836025229614329, 1.000000000000000000 ) ) 
 REPRESENTATION_ITEM ( '' )  );
#3424=EDGE_CURVE ( 'NONE', #145089, #128091, #166032, .T. ) ;
#3553=CARTESIAN_POINT ( 'NONE',  ( -18.40000000000000213, 70.35000000001159037, -56.87310748452436115 ) ) ;
#3605=DIRECTION ( 'NONE',  ( 1.186688945009009831E-16, 1.000000000000000000, 6.982962677686266711E-15 ) ) ;
#3627=ORIENTED_EDGE ( 'NONE', *, *, #30473, .T. ) ;
#3749=CARTESIAN_POINT ( 'NONE',  ( -16.82055514392378015, 66.05000000001153637, -48.69990555906626639 ) ) ;
#4059=VECTOR ( 'NONE', #190730, 1000.000000000000000 ) ;
#4127=CARTESIAN_POINT ( 'NONE',  ( -16.83199030136658081, 66.06935196689811107, -56.75070646186691903 ) ) ;
#4139=CARTESIAN_POINT ( 'NONE',  ( -16.82542659449980604, 66.06550010858417465, -56.77847188449814553 ) ) ;
#4295=CIRCLE ( 'NONE', #124940, 0.1999999999999987899 ) ;
#4654=ORIENTED_EDGE ( 'NONE', *, *, #72986, .T. ) ;
#4863=DIRECTION ( 'NONE',  ( 1.000000000000000000, 0.000000000000000000, 0.000000000000000000 ) ) ;
#4913=CARTESIAN_POINT ( 'NONE',  ( -18.41431012584569160, 64.51252797080344692, -60.29634349762607570 ) ) ;
#5112=AXIS2_PLACEMENT_3D ( 'NONE', #37838, #200737, #217709 ) ;
#5165=FACE_OUTER_BOUND ( 'NONE', #44928, .T. ) ;
#5397=CARTESIAN_POINT ( 'NONE',  ( -16.87333278164152617, 66.11739021543287720, -56.38993967837032528 ) ) ;
#5410=CARTESIAN_POINT ( 'NONE',  ( 16.87683809663750267, 66.05000000001157900, -56.87310748452439668 ) ) ;
#5444=ORIENTED_EDGE ( 'NONE', *, *, #234755, .F. ) ;
#5582=CARTESIAN_POINT ( 'NONE',  ( -18.40000000000000213, 64.51332499825393541, -60.27310748452440947 ) ) ;
#5753=ORIENTED_EDGE ( 'NONE', *, *, #221990, .F. ) ;
#5771=VERTEX_POINT ( 'NONE', #130815 ) ;
#5785=CARTESIAN_POINT ( 'NONE',  ( 18.54999999999999716, 67.25000000001149658, -48.67310748452438673 ) ) ;
#6044=CARTESIAN_POINT ( 'NONE',  ( -21.65000000000000213, 66.05000000001157900, -56.77310748452439526 ) ) ;
#6303=CARTESIAN_POINT ( 'NONE',  ( -16.84793658983433318, 66.05000000001152216, -48.75675416233475090 ) ) ;
#6335=DIRECTION ( 'NONE',  ( 0.000000000000000000, -6.982962677686266711E-15, 1.000000000000000000 ) ) ;
#6373=( NAMED_UNIT ( * ) PLANE_ANGLE_UNIT ( ) SI_UNIT ( $, .RADIAN. ) );
#6425=PLANE ( 'NONE',  #254044 ) ;
#6505=EDGE_CURVE ( 'NONE', #71110, #176580, #200639, .T. ) ;
#6598=CIRCLE ( 'NONE', #223076, 1.749999999999999778 ) ;
#6778=VECTOR ( 'NONE', #67739, 1000.000000000000000 ) ;
#6889=CARTESIAN_POINT ( 'NONE',  ( -17.11825945287482753, 65.95000000001158469, -56.77310748452439526 ) ) ;
#7053=CARTESIAN_POINT ( 'NONE',  ( -16.89797118371640039, 66.02361927736686198, -56.96040085208282733 ) ) ;
#7362=LINE ( 'NONE', #116736, #167353 ) ;
#7507=CARTESIAN_POINT ( 'NONE',  ( -12.68215100488889924, 66.60336962369382263, -51.61605009170610003 ) ) ;
#7601=EDGE_CURVE ( 'NONE', #128539, #96616, #67889, .T. ) ;
#7680=ORIENTED_EDGE ( 'NONE', *, *, #256341, .F. ) ;
#8104=EDGE_LOOP ( 'NONE', ( #9051, #232964, #127557, #58043, #78352 ) ) ;
#8173=CARTESIAN_POINT ( 'NONE',  ( -16.86445178670622980, 66.03778837089568299, -48.63233004640768087 ) ) ;
#8243=CARTESIAN_POINT ( 'NONE',  ( 23.24999999999999645, 64.25000000001159606, -56.87310748452439668 ) ) ;
#8277=( BOUNDED_SURFACE ( )  B_SPLINE_SURFACE ( 3, 2, ( 
 ( #34434, #151803, #252149 ),
 ( #91806, #113929, #214323 ),
 ( #35714, #158237, #198599 ),
 ( #241583, #390, #39571 ) ),
 .UNSPECIFIED., .F., .F., .F. ) 
 B_SPLINE_SURFACE_WITH_KNOTS ( ( 4, 4 ),
 ( 3, 3 ),
 ( 0.3000847527772385059, 0.5552748953338751958 ),
 ( 0.000000000000000000, 1.000000000000000000 ),
 .UNSPECIFIED. ) 
 GEOMETRIC_REPRESENTATION_ITEM ( )  RATIONAL_B_SPLINE_SURFACE ( (
 ( 1.000000000000000000, 0.9152888060719408525, 1.000000000000000000),
 ( 1.000000000000000000, 0.9104333467450420603, 1.000000000000000000),
 ( 1.000000000000000000, 0.9035312726220527946, 1.000000000000000000),
 ( 1.000000000000000000, 0.8946697475932202659, 1.000000000000000000) ) ) 
 REPRESENTATION_ITEM ( '' )  SURFACE ( )  );
#8482=VECTOR ( 'NONE', #159915, 1000.000000000000000 ) ;
#8628=AXIS2_PLACEMENT_3D ( 'NONE', #94802, #152248, #93520 ) ;
#9051=ORIENTED_EDGE ( 'NONE', *, *, #119754, .T. ) ;
#9136=ORIENTED_EDGE ( 'NONE', *, *, #207117, .F. ) ;
#9238=ORIENTED_EDGE ( 'NONE', *, *, #132402, .T. ) ;
#9351=ORIENTED_EDGE ( 'NONE', *, *, #130059, .F. ) ;
#9397=CARTESIAN_POINT ( 'NONE',  ( -16.94107738177415712, 65.98576071487495653, -56.97310748452439810 ) ) ;
#9627=AXIS2_PLACEMENT_3D ( 'NONE', #83593, #141050, #198439 ) ;
#9797=CARTESIAN_POINT ( 'NONE',  ( -18.34374000495060386, 64.52683809664912928, -60.27310748452440947 ) ) ;
#10009=EDGE_CURVE ( 'NONE', #211228, #68580, #120206, .T. ) ;
#10201=EDGE_LOOP ( 'NONE', ( #4654, #146788 ) ) ;
#10330=ADVANCED_FACE ( 'NONE', ( #91320 ), #95162, .F. ) ;
#10340=CARTESIAN_POINT ( 'NONE',  ( 22.88900146558018989, 67.29609520889877672, -60.27310748452438816 ) ) ;
#10363=DIRECTION ( 'NONE',  ( 0.000000000000000000, 1.000000000000000000, 6.982962677686266711E-15 ) ) ;
#10479=EDGE_CURVE ( 'NONE', #46675, #12212, #101545, .T. ) ;
#10533=CARTESIAN_POINT ( 'NONE',  ( -16.93388492042258875, 66.01145817749568323, -56.92365260771056512 ) ) ;
#10805=CARTESIAN_POINT ( 'NONE',  ( -16.77683809663752257, 66.05416425680736836, -48.68705650362859672 ) ) ;
#11023=ORIENTED_EDGE ( 'NONE', *, *, #203096, .T. ) ;
#11033=ORIENTED_EDGE ( 'NONE', *, *, #165153, .T. ) ;
#11128=ORIENTED_EDGE ( 'NONE', *, *, #97652, .F. ) ;
#11257=DIRECTION ( 'NONE',  ( 0.000000000000000000, -1.000000000000000000, -6.982962677686266711E-15 ) ) ;
#11305=CARTESIAN_POINT ( 'NONE',  ( -18.40000000000000213, 67.17743825834520521, -60.27310748452438816 ) ) ;
#11469=CARTESIAN_POINT ( 'NONE',  ( -16.94333152882356330, 66.00965798855385458, -48.63107595342290779 ) ) ;
#11668=CARTESIAN_POINT ( 'NONE',  ( 20.99999999999999645, 66.25000000001153921, -48.67310748452440095 ) ) ;
#11736=CARTESIAN_POINT ( 'NONE',  ( -18.40000000000000213, 64.51332499825382172, -45.27310748452440947 ) ) ;
#11834=CARTESIAN_POINT ( 'NONE',  ( -16.97048326478264713, 66.05000000001157900, -56.38200060439721284 ) ) ;
#11932=ORIENTED_EDGE ( 'NONE', *, *, #15096, .T. ) ;
#12110=CARTESIAN_POINT ( 'NONE',  ( -16.77732147262506146, 66.05403306739287927, -48.68661624124851528 ) ) ;
#12153=MECHANICAL_DESIGN_GEOMETRIC_PRESENTATION_REPRESENTATION('',(#191221),#257769);
#12212=VERTEX_POINT ( 'NONE', #6044 ) ;
#12224=CARTESIAN_POINT ( 'NONE',  ( -16.87036670365548474, 66.01058118070987746, -48.54354736722234520 ) ) ;
#12279=EDGE_CURVE ( 'NONE', #235449, #101287, #3274, .T. ) ;
#12593=ORIENTED_EDGE ( 'NONE', *, *, #119754, .F. ) ;
#12642=LINE ( 'NONE', #13911, #95851 ) ;
#12748=CARTESIAN_POINT ( 'NONE',  ( 12.29592348164039528, 66.64419340838141181, -53.23200495297823664 ) ) ;
#12944=LINE ( 'NONE', #52019, #72687 ) ;
#12949=DIRECTION ( 'NONE',  ( 0.000000000000000000, 6.982962677686266711E-15, -1.000000000000000000 ) ) ;
#13046=CARTESIAN_POINT ( 'NONE',  ( -16.87036670365548474, 66.01058118070987746, -48.54354736722234520 ) ) ;
#13073=VERTEX_POINT ( 'NONE', #28918 ) ;
#13233=LINE ( 'NONE', #189292, #239421 ) ;
#13299=VERTEX_POINT ( 'NONE', #124770 ) ;
#13360=VECTOR ( 'NONE', #74071, 1000.000000000000000 ) ;
#13395=EDGE_CURVE ( 'NONE', #120974, #205644, #126477, .T. ) ;
#13534=CARTESIAN_POINT ( 'NONE',  ( 20.27550659511088682, 66.78395627750275310, -60.27310748452438816 ) ) ;
#13680=B_SPLINE_CURVE_WITH_KNOTS ( 'NONE', 3,
 ( #13686, #31995, #134891, #110214, #72404, #54094, #132350, #91941, #194919, #231473, #252284, #192335, #133637 ),
 .UNSPECIFIED., .F., .F.,
 ( 4, 3, 3, 3, 4 ),
 ( 1.084445006577768218E-16, 1.946463881814412345E-05, 3.922356109944399394E-05, 4.215060953238735362E-05, 4.415117091092665805E-05 ),
 .UNSPECIFIED. ) ;
#13686=CARTESIAN_POINT ( 'NONE',  ( -16.81744102076749314, 66.05000000001157900, -56.87310748452438958 ) ) ;
#13802=DIRECTION ( 'NONE',  ( 1.073024830501117725E-15, 6.982962677686266711E-15, -1.000000000000000000 ) ) ;
#13868=DIRECTION ( 'NONE',  ( 1.000000000000000000, 0.000000000000000000, 0.000000000000000000 ) ) ;
#13911=CARTESIAN_POINT ( 'NONE',  ( 20.27550659511088682, 66.78395627750275310, -60.27310748452438816 ) ) ;
#13939=CARTESIAN_POINT ( 'NONE',  ( -15.06720934482788010, 66.58230930894843880, -51.38150678775980396 ) ) ;
#14034=CARTESIAN_POINT ( 'NONE',  ( -16.86337532320262156, 66.02003279578721617, -56.97203195350720506 ) ) ;
#14077=LINE ( 'NONE', #93597, #13360 ) ;
#14079=EDGE_CURVE ( 'NONE', #190074, #48902, #230928, .T. ) ;
#14108=DIRECTION ( 'NONE',  ( 0.000000000000000000, 6.982962677686266711E-15, -1.000000000000000000 ) ) ;
#14243=EDGE_CURVE ( 'NONE', #63364, #229182, #93131, .T. ) ;
#14346=( BOUNDED_SURFACE ( )  B_SPLINE_SURFACE ( 3, 2, ( 
 ( #102732, #4913, #242259 ),
 ( #243552, #240997, #144426 ),
 ( #64908, #45356, #165305 ),
 ( #205701, #25792, #244829 ) ),
 .UNSPECIFIED., .F., .F., .F. ) 
 B_SPLINE_SURFACE_WITH_KNOTS ( ( 4, 4 ),
 ( 3, 3 ),
 ( 5.727910411845712702, 5.983100554402349225 ),
 ( 0.000000000000000000, 1.000000000000000000 ),
 .UNSPECIFIED. ) 
 GEOMETRIC_REPRESENTATION_ITEM ( )  RATIONAL_B_SPLINE_SURFACE ( (
 ( 1.000000000000000000, 0.8946697475932264831, 1.000000000000000000),
 ( 1.000000000000000000, 0.9035312726220544599, 1.000000000000000000),
 ( 1.000000000000000000, 0.9104333467450480555, 1.000000000000000000),
 ( 1.000000000000000000, 0.9152888060719390761, 1.000000000000000000) ) ) 
 REPRESENTATION_ITEM ( '' )  SURFACE ( )  );
#14571=DIRECTION ( 'NONE',  ( 0.000000000000000000, -6.789366196018718420E-15, 1.000000000000000000 ) ) ;
#14611=VERTEX_POINT ( 'NONE', #174232 ) ;
#15062=CARTESIAN_POINT ( 'NONE',  ( -16.92507428761701505, 66.05000000001157900, -56.80971002490283439 ) ) ;
#15096=EDGE_CURVE ( 'NONE', #250894, #162196, #186420, .T. ) ;
#15246=EDGE_CURVE ( 'NONE', #235449, #197047, #209824, .T. ) ;
#15274=CARTESIAN_POINT ( 'NONE',  ( -21.64999999999999858, 65.95000000001152785, -48.67310748452439384 ) ) ;
#15296=CYLINDRICAL_SURFACE ( 'NONE', #8628, 1.749999999999999778 ) ;
#15520=EDGE_CURVE ( 'NONE', #229182, #181669, #192508, .T. ) ;
#15577=EDGE_LOOP ( 'NONE', ( #206334, #87764, #247105, #116318 ) ) ;
#15614=ORIENTED_EDGE ( 'NONE', *, *, #6505, .F. ) ;
#16096=CARTESIAN_POINT ( 'NONE',  ( -18.40000000000000213, 64.66825945288634614, -48.67310748452440805 ) ) ;
#16120=LINE ( 'NONE', #175218, #160198 ) ;
#16468=VERTEX_POINT ( 'NONE', #18064 ) ;
#16521=VERTEX_POINT ( 'NONE', #223957 ) ;
#16531=DIRECTION ( 'NONE',  ( 1.000000000000000000, 0.000000000000000000, 0.000000000000000000 ) ) ;
#16691=( BOUNDED_CURVE ( )  B_SPLINE_CURVE ( 3, ( #194758, #249581, #214297, #70966 ),
 .UNSPECIFIED., .F., .F. ) 
 B_SPLINE_CURVE_WITH_KNOTS ( ( 4, 4 ),
 ( 3.432212674861196522, 3.693332928900582068 ),
 .UNSPECIFIED. ) 
 CURVE ( )  GEOMETRIC_REPRESENTATION_ITEM ( )  RATIONAL_B_SPLINE_CURVE ( ( 1.000000000000000000, 0.9943260843901261525, 0.9943260843901261525, 1.000000000000000000 ) ) 
 REPRESENTATION_ITEM ( '' )  );
#16979=SURFACE_SIDE_STYLE ('',( #177354 ) ) ;
#17187=ORIENTED_EDGE ( 'NONE', *, *, #53915, .T. ) ;
#17190=LINE ( 'NONE', #193249, #144448 ) ;
#17364=CARTESIAN_POINT ( 'NONE',  ( 12.93279065517212345, 66.58230930894843880, -51.38150678775981106 ) ) ;
#17382=FACE_OUTER_BOUND ( 'NONE', #92491, .T. ) ;
#17688=CARTESIAN_POINT ( 'NONE',  ( -15.70407651835961005, 66.64419340838139760, -53.23200495297821533 ) ) ;
#17826=CARTESIAN_POINT ( 'NONE',  ( -21.65000000000000213, 68.75000000001159606, -56.87310748452436826 ) ) ;
#17854=CARTESIAN_POINT ( 'NONE',  ( -16.93234230245721861, 66.00189262946443591, -48.60541720285813483 ) ) ;
#18064=CARTESIAN_POINT ( 'NONE',  ( 22.88900146558018989, 67.29609520889870566, -48.67310748452439384 ) ) ;
#18185=EDGE_CURVE ( 'NONE', #2351, #91508, #166146, .T. ) ;
#18382=ORIENTED_EDGE ( 'NONE', *, *, #90651, .T. ) ;
#18484=PLANE ( 'NONE',  #166688 ) ;
#18492=EDGE_CURVE ( 'NONE', #197047, #99410, #13680, .T. ) ;
#18639=CARTESIAN_POINT ( 'NONE',  ( 15.39170923737819763, 66.61047060254480812, -51.70599957163072702 ) ) ;
#18795=VECTOR ( 'NONE', #195704, 1000.000000000000000 ) ;
#18879=VECTOR ( 'NONE', #104918, 1000.000000000000000 ) ;
#18952=FACE_OUTER_BOUND ( 'NONE', #224335, .T. ) ;
#18981=ORIENTED_EDGE ( 'NONE', *, *, #211864, .F. ) ;
#19024=VERTEX_POINT ( 'NONE', #45471 ) ;
#19362=VECTOR ( 'NONE', #78832, 1000.000000000000000 ) ;
#19464=CARTESIAN_POINT ( 'NONE',  ( -16.80100914604134843, 66.05685090590795028, -48.70606335723675073 ) ) ;
#19877=CARTESIAN_POINT ( 'NONE',  ( -16.85722902420149083, 66.05000000001159322, -56.75756001075396995 ) ) ;
#19967=ORIENTED_EDGE ( 'NONE', *, *, #85312, .F. ) ;
#19990=VERTEX_POINT ( 'NONE', #58943 ) ;
#20176=CYLINDRICAL_SURFACE ( 'NONE', #44841, 14.30833333333333890 ) ;
#20747=ORIENTED_EDGE ( 'NONE', *, *, #29972, .T. ) ;
#20793=AXIS2_PLACEMENT_3D ( 'NONE', #128837, #71440, #187540 ) ;
#20968=DIRECTION ( 'NONE',  ( -1.652117596168391700E-15, 1.000000000000000000, 6.982962677686266711E-15 ) ) ;
#21371=PRODUCT_DEFINITION ( 'UNKNOWN', '', #73925, #139182 ) ;
#21498=CARTESIAN_POINT ( 'NONE',  ( 20.99999999999999645, 66.25000000001153921, -48.67310748452440095 ) ) ;
#21543=DIRECTION ( 'NONE',  ( -1.000000000000000000, -1.652117596168391700E-15, -1.153667551319263085E-29 ) ) ;
#21570=CARTESIAN_POINT ( 'NONE',  ( -13.12432614554023225, 66.56923500458923115, -54.29257008977393895 ) ) ;
#21600=CARTESIAN_POINT ( 'NONE',  ( -16.94062896051973865, 66.00728089491089179, -56.92059094240559602 ) ) ;
#21782=EDGE_LOOP ( 'NONE', ( #127147, #108894, #28485, #217704 ) ) ;
#21807=CARTESIAN_POINT ( 'NONE',  ( -18.40000000000000213, 64.66825945288634614, -48.67310748452440805 ) ) ;
#22237=LINE ( 'NONE', #118766, #126460 ) ;
#22264=ORIENTED_EDGE ( 'NONE', *, *, #165632, .T. ) ;
#22343=VERTEX_POINT ( 'NONE', #150087 ) ;
#22366=CARTESIAN_POINT ( 'NONE',  ( -16.89060415895971090, 66.04877923720935939, -56.87718726025393323 ) ) ;
#22394=ORIENTED_EDGE ( 'NONE', *, *, #53194, .T. ) ;
#22440=CARTESIAN_POINT ( 'NONE',  ( -16.85939591225059075, 66.09477352162372199, -56.56303923805535305 ) ) ;
#22736=EDGE_CURVE ( 'NONE', #249506, #146300, #145365, .T. ) ;
#22941=CARTESIAN_POINT ( 'NONE',  ( -23.25000000000000355, 64.25000000001159606, -56.87310748452440379 ) ) ;
#22980=EDGE_LOOP ( 'NONE', ( #9351, #70023, #243865, #215088 ) ) ;
#23154=FACE_OUTER_BOUND ( 'NONE', #63300, .T. ) ;
#23348=CARTESIAN_POINT ( 'NONE',  ( -16.77431908686106610, 66.05419424549353380, -48.68726826687415610 ) ) ;
#23661=CARTESIAN_POINT ( 'NONE',  ( -16.87383368123029825, 66.05000000001157900, -56.87310748452438958 ) ) ;
#23669=CARTESIAN_POINT ( 'NONE',  ( -21.64999999999999858, 66.65000000001158753, -56.87310748452438958 ) ) ;
#23948=CARTESIAN_POINT ( 'NONE',  ( -20.65000000000000568, 68.75000000001161027, -60.27310748452437394 ) ) ;
#24079=CARTESIAN_POINT ( 'NONE',  ( -18.40000000000000213, 64.25000000001159606, -56.87310748452440379 ) ) ;
#24274=LINE ( 'NONE', #184604, #72301 ) ;
#24290=ORIENTED_EDGE ( 'NONE', *, *, #107805, .T. ) ;
#24297=DIRECTION ( 'NONE',  ( -0.7071067811865487940, -0.7071067811865463515, -4.937700262164522799E-15 ) ) ;
#24371=ADVANCED_FACE ( 'NONE', ( #5165 ), #102998, .F. ) ;
#24568=ORIENTED_EDGE ( 'NONE', *, *, #89942, .T. ) ;
#24631=CARTESIAN_POINT ( 'NONE',  ( -16.80070461187883879, 66.05000000001155058, -48.67007131368379191 ) ) ;
#25021=CARTESIAN_POINT ( 'NONE',  ( -16.87683809663752754, 66.13411015068078314, -56.25568067745533796 ) ) ;
#25178=CARTESIAN_POINT ( 'NONE',  ( -17.11825945287481687, 66.05000000001153637, -48.77310748452439526 ) ) ;
#25647=CARTESIAN_POINT ( 'NONE',  ( 15.74999999999999645, 66.15000000001155911, -52.77310748452440237 ) ) ;
#25711=EDGE_CURVE ( 'NONE', #68580, #256608, #60530, .T. ) ;
#25792=CARTESIAN_POINT ( 'NONE',  ( -16.91256925476572093, 66.01426884188337851, -56.99074997352967387 ) ) ;
#26087=DIRECTION ( 'NONE',  ( 0.000000000000000000, -6.982962677686266711E-15, 1.000000000000000000 ) ) ;
#26175=CARTESIAN_POINT ( 'NONE',  ( -18.40000000000000213, 70.35000000001153353, -48.67310748452436542 ) ) ;
#26402=CARTESIAN_POINT ( 'NONE',  ( -16.89081410710458542, 66.04868147016441071, -48.66870156468802833 ) ) ;
#26658=VECTOR ( 'NONE', #65197, 1000.000000000000000 ) ;
#26906=CARTESIAN_POINT ( 'NONE',  ( -18.40000000000000213, 64.25000000001153921, -48.67310748452440805 ) ) ;
#26949=ORIENTED_EDGE ( 'NONE', *, *, #110871, .F. ) ;
#27107=CARTESIAN_POINT ( 'NONE',  ( -12.33960340485504226, 66.63925083009645789, -52.20853734391712919 ) ) ;
#27424=ORIENTED_EDGE ( 'NONE', *, *, #150607, .T. ) ;
#27559=CARTESIAN_POINT ( 'NONE',  ( -17.11825945287482753, 66.05000000001159322, -56.87310748452439668 ) ) ;
#27778=DIRECTION ( 'NONE',  ( 0.000000000000000000, 0.000000000000000000, 1.000000000000000000 ) ) ;
#28018=CARTESIAN_POINT ( 'NONE',  ( -18.39999999999999858, 64.52683809664912928, -60.19716141771643692 ) ) ;
#28261=ORIENTED_EDGE ( 'NONE', *, *, #91991, .F. ) ;
#28399=CARTESIAN_POINT ( 'NONE',  ( -15.15564720441980562, 66.58929125296442919, -51.45389907868027990 ) ) ;
#28485=ORIENTED_EDGE ( 'NONE', *, *, #97652, .T. ) ;
#28543=LINE ( 'NONE', #244965, #140450 ) ;
#28918=CARTESIAN_POINT ( 'NONE',  ( 23.24999999999999645, 64.25000000001153921, -48.67310748452441516 ) ) ;
#28979=ORIENTED_EDGE ( 'NONE', *, *, #192763, .T. ) ;
#29115=DIRECTION ( 'NONE',  ( 1.000000000000000000, 0.000000000000000000, 0.000000000000000000 ) ) ;
#29116=CYLINDRICAL_SURFACE ( 'NONE', #78983, 0.1999999999999987899 ) ;
#29566=CARTESIAN_POINT ( 'NONE',  ( 23.24999999999999645, 70.35000000001153353, -48.67310748452437252 ) ) ;
#29673=CARTESIAN_POINT ( 'NONE',  ( -13.77083647240106501, 66.54258906972138732, -51.02319157577811382 ) ) ;
#29972=EDGE_CURVE ( 'NONE', #206624, #57410, #12944, .T. ) ;
#30116=SHAPE_DEFINITION_REPRESENTATION ( #163737, #100031 ) ;
#30370=CARTESIAN_POINT ( 'NONE',  ( -17.01825945287481545, 66.05000000001153637, -48.77310748452439526 ) ) ;
#30392=EDGE_CURVE ( 'NONE', #181669, #206624, #218476, .T. ) ;
#30473=EDGE_CURVE ( 'NONE', #224622, #146300, #113247, .T. ) ;
#30506=ORIENTED_EDGE ( 'NONE', *, *, #234868, .T. ) ;
#30577=DIRECTION ( 'NONE',  ( -1.073024830501117725E-15, -6.982962677686266711E-15, 1.000000000000000000 ) ) ;
#30702=ORIENTED_EDGE ( 'NONE', *, *, #80194, .F. ) ;
#30710=EDGE_CURVE ( 'NONE', #143115, #16521, #93688, .T. ) ;
#30813=CARTESIAN_POINT ( 'NONE',  ( -17.11825945287482753, 65.95000000001159890, -56.87310748452438958 ) ) ;
#31037=CARTESIAN_POINT ( 'NONE',  ( 13.22261339317536866, 66.56344716000714357, -54.34515201176409960 ) ) ;
#31173=FACE_OUTER_BOUND ( 'NONE', #87760, .T. ) ;
#31246=VECTOR ( 'NONE', #86431, 1000.000000000000000 ) ;
#31304=ORIENTED_EDGE ( 'NONE', *, *, #192762, .F. ) ;
#31403=CARTESIAN_POINT ( 'NONE',  ( -16.97683809663752186, 66.05000000001157900, -56.12074346632790878 ) ) ;
#31800=DIRECTION ( 'NONE',  ( -1.000000000000000000, 0.000000000000000000, -0.000000000000000000 ) ) ;
#31937=ORIENTED_EDGE ( 'NONE', *, *, #10479, .F. ) ;
#31995=CARTESIAN_POINT ( 'NONE',  ( -16.81095280782811230, 66.05000000001157900, -56.87310748452526354 ) ) ;
#32122=ORIENTED_EDGE ( 'NONE', *, *, #91262, .F. ) ;
#32314=CARTESIAN_POINT ( 'NONE',  ( 14.45204356427542081, 66.54933111084405084, -54.46756099431704712 ) ) ;
#32518=CARTESIAN_POINT ( 'NONE',  ( -23.25000000000000355, 64.25000000001161027, -60.27310748452440947 ) ) ;
#32606=CARTESIAN_POINT ( 'NONE',  ( -18.38817693311004575, 64.51850848411172024, -45.27310748452440947 ) ) ;
#32698=PLANE ( 'NONE',  #109754 ) ;
#32732=ORIENTED_EDGE ( 'NONE', *, *, #22736, .T. ) ;
#33095=CARTESIAN_POINT ( 'NONE',  ( -16.87304349924914604, 66.03825492205433534, -48.63404080947914565 ) ) ;
#33164=CARTESIAN_POINT ( 'NONE',  ( -16.87683809663752399, 54.76195096157850628, -56.87310748452446774 ) ) ;
#33232=CARTESIAN_POINT ( 'NONE',  ( -17.78043020864320667, 65.14640788800591054, -59.18615665024461947 ) ) ;
#33489=DIRECTION ( 'NONE',  ( 1.000000000000000000, 0.000000000000000000, 0.000000000000000000 ) ) ;
#33541=CARTESIAN_POINT ( 'NONE',  ( -14.77538296656415717, 66.56333706821246210, -51.20007075222951443 ) ) ;
#33634=CARTESIAN_POINT ( 'NONE',  ( -16.86578989773641979, 66.01519019875277650, -56.98777237114663308 ) ) ;
#33654=PLANE ( 'NONE',  #225195 ) ;
#33836=ADVANCED_FACE ( 'NONE', ( #166890 ), #66470, .F. ) ;
#33897=CARTESIAN_POINT ( 'NONE',  ( -18.34374000495059676, 64.52683809664901560, -45.27310748452439526 ) ) ;
#33956=DIRECTION ( 'NONE',  ( -1.073024830501117725E-15, 6.982962677686266711E-15, -1.000000000000000000 ) ) ;
#34265=SURFACE_SIDE_STYLE ('',( #151640 ) ) ;
#34415=EDGE_CURVE ( 'NONE', #99410, #99179, #149144, .T. ) ;
#34434=CARTESIAN_POINT ( 'NONE',  ( -16.94107738177414291, 65.98576071487489969, -48.57310748452439952 ) ) ;
#34659=DIRECTION ( 'NONE',  ( 1.000000000000000000, 0.000000000000000000, 0.000000000000000000 ) ) ;
#34715=AXIS2_PLACEMENT_3D ( 'NONE', #104783, #106075, #228647 ) ;
#34856=DIRECTION ( 'NONE',  ( 0.000000000000000000, 1.000000000000000000, 6.982962677686266711E-15 ) ) ;
#35073=ORIENTED_EDGE ( 'NONE', *, *, #110832, .F. ) ;
#35106=DIRECTION ( 'NONE',  ( 1.073024830501117725E-15, -6.982962677686266711E-15, 1.000000000000000000 ) ) ;
#35253=CARTESIAN_POINT ( 'NONE',  ( 13.99999999999999822, 66.15000000001155911, -52.77310748452440237 ) ) ;
#35331=VECTOR ( 'NONE', #207526, 1000.000000000000000 ) ;
#35522=ORIENTED_EDGE ( 'NONE', *, *, #191369, .F. ) ;
#35714=CARTESIAN_POINT ( 'NONE',  ( -17.80356949364257702, 65.12326860300646558, -46.31003446030745607 ) ) ;
#35748=B_SPLINE_CURVE_WITH_KNOTS ( 'NONE', 3,
 ( #240116, #22366, #99287, #224383, #142283, #101851, #120199, #243951, #23661, #103143 ),
 .UNSPECIFIED., .F., .F.,
 ( 4, 3, 3, 4 ),
 ( 1.957469226477651626E-15, 8.145022132833432322E-06, 1.905645951092475529E-05, 2.061107371225855961E-05 ),
 .UNSPECIFIED. ) ;
#35944=B_SPLINE_CURVE_WITH_KNOTS ( 'NONE', 3,
 ( #125488, #246708, #68080, #224575, #128061, #182909, #26402, #245450, #244133, #207610 ),
 .UNSPECIFIED., .F., .F.,
 ( 4, 3, 3, 4 ),
 ( 0.000000000000000000, 1.004626015991446001E-05, 1.831183478183186726E-05, 2.062343583996000413E-05 ),
 .UNSPECIFIED. ) ;
#35958=ORIENTED_EDGE ( 'NONE', *, *, #38179, .T. ) ;
#36030=CARTESIAN_POINT ( 'NONE',  ( -14.00000000000000178, 66.15000000001155911, -52.77310748452439526 ) ) ;
#36152=CARTESIAN_POINT ( 'NONE',  ( -16.94333152886236249, 66.00965798856108790, -56.91513901557880217 ) ) ;
#36371=ORIENTED_EDGE ( 'NONE', *, *, #91991, .T. ) ;
#36478=( BOUNDED_SURFACE ( )  B_SPLINE_SURFACE ( 3, 2, ( 
 ( #44565, #180231, #198492 ),
 ( #237631, #103224, #25021 ),
 ( #61559, #201063, #5397 ),
 ( #163234, #1563, #121564 ),
 ( #2842, #81098, #181522 ),
 ( #160689, #19877, #240205 ),
 ( #182807, #184063, #4139 ),
 ( #101932, #84928, #124112 ),
 ( #99370, #138491, #141100 ),
 ( #220633, #161961, #40745 ) ),
 .UNSPECIFIED., .F., .F., .F. ) 
 B_SPLINE_SURFACE_WITH_KNOTS ( ( 4, 2, 2, 2, 4 ),
 ( 3, 3 ),
 ( 0.002161241639767792072, 0.002579950749617453305, 0.002789305304542283922, 0.002893982582004699447, 0.002998659859467114538 ),
 ( 0.000000000000000000, 1.000000000000000000 ),
 .UNSPECIFIED. ) 
 GEOMETRIC_REPRESENTATION_ITEM ( )  RATIONAL_B_SPLINE_SURFACE ( (
 ( 1.000000000000000000, 0.7071067811864985009, 1.000000000000000000),
 ( 1.000000000000000000, 0.7632447400665891557, 1.000000000000000000),
 ( 1.000000000000000000, 0.8158073005106942777, 1.000000000000000000),
 ( 1.000000000000000000, 0.8906973462396924335, 1.000000000000000000),
 ( 1.000000000000000000, 0.9149408947797951219, 1.000000000000000000),
 ( 1.000000000000000000, 0.9493368785276811161, 1.000000000000000000),
 ( 1.000000000000000000, 0.9605194247156072507, 1.000000000000000000),
 ( 1.000000000000000000, 0.9803630264781720838, 1.000000000000000000),
 ( 1.000000000000000000, 0.9900844824270710332, 1.000000000000000000),
 ( 1.000000000000000000, 0.9894588281429290699, 1.000000000000000000) ) ) 
 REPRESENTATION_ITEM ( '' )  SURFACE ( )  );
#36481=CARTESIAN_POINT ( 'NONE',  ( -16.79140778683510504, 66.05505840115696969, -48.69337025075360259 ) ) ;
#36563=FILL_AREA_STYLE_COLOUR ( '', #145386 ) ;
#36596=DIRECTION ( 'NONE',  ( -1.000000000000000000, 0.000000000000000000, 0.000000000000000000 ) ) ;
#36659=ORIENTED_EDGE ( 'NONE', *, *, #250280, .T. ) ;
#36740=ORIENTED_EDGE ( 'NONE', *, *, #115048, .T. ) ;
#36828=ORIENTED_EDGE ( 'NONE', *, *, #173338, .T. ) ;
#36918=ORIENTED_EDGE ( 'NONE', *, *, #85312, .T. ) ;
#36934=CLOSED_SHELL ( 'NONE', ( #79948, #107676, #41369, #217398, #152620, #219378, #112841, #59185, #38821, #255864, #122761, #168584, #33836, #233655, #46341, #61137, #115523, #226844, #226917, #103127, #86989, #71687, #91185, #122129, #41386, #131259, #10330, #55106, #1766, #68910, #90326, #119124, #178924, #151361, #213782, #118985, #24371, #92409, #227987, #129657, #192615, #110201, #156343, #142198, #59309, #217145, #221575, #64756, #204344, #148407, #253722, #97249, #196693 ) ) ;
#36956=CARTESIAN_POINT ( 'NONE',  ( 14.88075390448864610, 66.56831044948744136, -51.24381745228834006 ) ) ;
#37266=FACE_OUTER_BOUND ( 'NONE', #257672, .T. ) ;
#37588=VERTEX_POINT ( 'NONE', #152957 ) ;
#37600=FACE_OUTER_BOUND ( 'NONE', #192363, .T. ) ;
#37615=B_SPLINE_CURVE_WITH_KNOTS ( 'NONE', 3,
 ( #154838, #234337, #96101, #55667, #156127, #235618, #116971, #196493, #17854, #97365, #51835, #131390, #210938, #81652, #101207, #238182 ),
 .UNSPECIFIED., .F., .F.,
 ( 4, 3, 3, 3, 3, 4 ),
 ( 0.000000000000000000, 1.810570668010038676E-05, 2.740575833571286165E-05, 4.256816319435689587E-05, 5.213463471024805661E-05, 6.641585710717877651E-05 ),
 .UNSPECIFIED. ) ;
#37624=VECTOR ( 'NONE', #29115, 1000.000000000000000 ) ;
#37759=CARTESIAN_POINT ( 'NONE',  ( -16.87372397896796272, 66.11940046336980004, -49.17238297448864870 ) ) ;
#37802=DIRECTION ( 'NONE',  ( -0.000000000000000000, -6.982962677686266711E-15, 1.000000000000000000 ) ) ;
#37838=CARTESIAN_POINT ( 'NONE',  ( 20.04999999999999716, 67.25000000001155342, -56.87310748452438247 ) ) ;
#37863=CARTESIAN_POINT ( 'NONE',  ( -16.97683809663752186, 66.15000000001158753, -56.12074346632790878 ) ) ;
#38083=DIRECTION ( 'NONE',  ( 0.7071067811865493491, -0.7071067811865456854, -4.937700262164518065E-15 ) ) ;
#38162=VECTOR ( 'NONE', #218773, 1000.000000000000000 ) ;
#38179=EDGE_CURVE ( 'NONE', #163978, #230076, #219141, .T. ) ;
#38288=CARTESIAN_POINT ( 'NONE',  ( -23.25000000000000355, 66.05000000001160743, -60.27310748452439526 ) ) ;
#38297=AXIS2_PLACEMENT_3D ( 'NONE', #229598, #193047, #73123 ) ;
#38314=DIRECTION ( 'NONE',  ( -1.000000000000000000, -0.000000000000000000, -0.000000000000000000 ) ) ;
#38439=ORIENTED_EDGE ( 'NONE', *, *, #207117, .T. ) ;
#38556=CARTESIAN_POINT ( 'NONE',  ( -15.06774609480955363, 66.58234804117054750, -54.16432009208396892 ) ) ;
#38821=ADVANCED_FACE ( 'NONE', ( #107380 ), #169982, .F. ) ;
#38872=CYLINDRICAL_SURFACE ( 'NONE', #168703, 1.500000000000001332 ) ;
#39047=CARTESIAN_POINT ( 'NONE',  ( -16.87683809663752399, 66.13411015067963206, -49.29053429159418442 ) ) ;
#39116=PRESENTATION_STYLE_ASSIGNMENT (( #76925 ) ) ;
#39157=ORIENTED_EDGE ( 'NONE', *, *, #211864, .T. ) ;
#39280=EDGE_LOOP ( 'NONE', ( #76657, #214846, #219029, #76127 ) ) ;
#39524=CARTESIAN_POINT ( 'NONE',  ( 15.07585980824113747, 66.58236703690523939, -51.37415901879214175 ) ) ;
#39571=CARTESIAN_POINT ( 'NONE',  ( -18.37013991200266005, 64.50025238379953407, -45.23008447400728471 ) ) ;
#39625=CARTESIAN_POINT ( 'NONE',  ( -33.72168855820451938, 66.05000000001156479, -56.87310748452444642 ) ) ;
#39759=FACE_BOUND ( 'NONE', #45272, .T. ) ;
#39864=CARTESIAN_POINT ( 'NONE',  ( -15.15766958671842701, 66.58946139148265786, -54.09041948738348538 ) ) ;
#40563=ORIENTED_EDGE ( 'NONE', *, *, #45161, .F. ) ;
#40676=PLANE ( 'NONE',  #54160 ) ;
#40733=CARTESIAN_POINT ( 'NONE',  ( -16.77683809663752257, 66.05416425680742520, -56.85915846542017960 ) ) ;
#40745=CARTESIAN_POINT ( 'NONE',  ( -16.77431908686106965, 66.05419424549359064, -56.85894670217464153 ) ) ;
#41300=CARTESIAN_POINT ( 'NONE',  ( -16.89268316805466341, 66.04827818676939444, -56.87885996306994230 ) ) ;
#41369=ADVANCED_FACE ( 'NONE', ( #18952 ), #239303, .F. ) ;
#41386=ADVANCED_FACE ( 'NONE', ( #37266 ), #116779, .F. ) ;
#41660=CARTESIAN_POINT ( 'NONE',  ( -16.84421487269768747, 66.05000000001159322, -56.85360536207942772 ) ) ;
#41852=ORIENTED_EDGE ( 'NONE', *, *, #61977, .F. ) ;
#41994=CARTESIAN_POINT ( 'NONE',  ( -18.40000000000000213, 64.52683809664901560, -45.27310748452439526 ) ) ;
#42215=ORIENTED_EDGE ( 'NONE', *, *, #48549, .F. ) ;
#42403=CARTESIAN_POINT ( 'NONE',  ( -12.29659703204451660, 66.64411154550899141, -53.23446458774639467 ) ) ;
#42695=EDGE_CURVE ( 'NONE', #254423, #99179, #68337, .T. ) ;
#42890=EDGE_CURVE ( 'NONE', #241094, #22343, #133194, .T. ) ;
#43438=CARTESIAN_POINT ( 'NONE',  ( -16.95709691156382348, 66.05000000001152216, -48.68316504703488334 ) ) ;
#43619=ORIENTED_EDGE ( 'NONE', *, *, #45885, .T. ) ;
#43652=AXIS2_PLACEMENT_3D ( 'NONE', #13534, #213004, #250834 ) ;
#43688=AXIS2_PLACEMENT_3D ( 'NONE', #65905, #163728, #204116 ) ;
#43784=B_SPLINE_CURVE_WITH_KNOTS ( 'NONE', 3,
 ( #187658, #148516, #247605, #68996, #183786, #164233, #228050 ),
 .UNSPECIFIED., .F., .F.,
 ( 4, 3, 4 ),
 ( 0.000000000000000000, 4.520325912680430423E-05, 5.794988040901218388E-05 ),
 .UNSPECIFIED. ) ;
#43920=LINE ( 'NONE', #25647, #131095 ) ;
#44176=CARTESIAN_POINT ( 'NONE',  ( -16.83558968593862915, 66.05000000001153637, -48.68541267214110491 ) ) ;
#44282=ORIENTED_EDGE ( 'NONE', *, *, #13395, .F. ) ;
#44296=DIRECTION ( 'NONE',  ( 1.000000000000000000, 0.000000000000000000, 0.000000000000000000 ) ) ;
#44453=DIRECTION ( 'NONE',  ( 0.000000000000000000, 0.000000000000000000, 1.000000000000000000 ) ) ;
#44550=DIRECTION ( 'NONE',  ( 0.000000000000000000, 6.982962677686266711E-15, -1.000000000000000000 ) ) ;
#44556=CARTESIAN_POINT ( 'NONE',  ( -16.78493832629887450, 66.05416425680742520, -56.85915846542017249 ) ) ;
#44558=DIRECTION ( 'NONE',  ( 1.020425574104004196E-15, 6.982962677686266711E-15, -1.000000000000000000 ) ) ;
#44565=CARTESIAN_POINT ( 'NONE',  ( -16.97683809663752186, 66.05000000001157900, -56.12074346632790878 ) ) ;
#44841=AXIS2_PLACEMENT_3D ( 'NONE', #140090, #179266, #80095 ) ;
#44861=DIRECTION ( 'NONE',  ( -0.000000000000000000, 6.982962677686266711E-15, -1.000000000000000000 ) ) ;
#44900=DIRECTION ( 'NONE',  ( 1.073024830501117725E-15, -6.982962677686266711E-15, 1.000000000000000000 ) ) ;
#44928=EDGE_LOOP ( 'NONE', ( #83807, #256650, #159313, #65950 ) ) ;
#44947=EDGE_CURVE ( 'NONE', #96616, #181669, #212930, .T. ) ;
#45161=EDGE_CURVE ( 'NONE', #214271, #13299, #98912, .T. ) ;
#45272=EDGE_LOOP ( 'NONE', ( #240935, #108991 ) ) ;
#45356=CARTESIAN_POINT ( 'NONE',  ( -17.27223548802019693, 65.65460260862890607, -58.15671366372658468 ) ) ;
#45445=CARTESIAN_POINT ( 'NONE',  ( -16.87333278164147288, 66.11739021543263561, -49.15627529067739943 ) ) ;
#45471=CARTESIAN_POINT ( 'NONE',  ( 18.54999999999999716, 67.25000000001155342, -56.87310748452438247 ) ) ;
#45528=ORIENTED_EDGE ( 'NONE', *, *, #110442, .F. ) ;
#45553=( BOUNDED_CURVE ( )  B_SPLINE_CURVE ( 3, ( #142690, #81418, #160998, #601 ),
 .UNSPECIFIED., .F., .F. ) 
 B_SPLINE_CURVE_WITH_KNOTS ( ( 4, 4 ),
 ( 1.570796326794908992, 2.617993877991515284 ),
 .UNSPECIFIED. ) 
 CURVE ( )  GEOMETRIC_REPRESENTATION_ITEM ( )  RATIONAL_B_SPLINE_CURVE ( ( 1.000000000000000000, 0.9106836025229576581, 0.9106836025229576581, 1.000000000000000000 ) ) 
 REPRESENTATION_ITEM ( '' )  );
#45783=VERTEX_POINT ( 'NONE', #256128 ) ;
#45829=LINE ( 'NONE', #152342, #206479 ) ;
#45885=EDGE_CURVE ( 'NONE', #122321, #105113, #143946, .T. ) ;
#45925=CARTESIAN_POINT ( 'NONE',  ( 15.74999999999999645, 66.65000000001155911, -52.77310748452439526 ) ) ;
#45993=CARTESIAN_POINT ( 'NONE',  ( -17.01764560440427942, 66.05000000001153637, -48.77310748373898264 ) ) ;
#46341=ADVANCED_FACE ( 'NONE', ( #248852 ), #113187, .F. ) ;
#46675=VERTEX_POINT ( 'NONE', #128593 ) ;
#46687=CIRCLE ( 'NONE', #59134, 1.749999999999998002 ) ;
#47053=CIRCLE ( 'NONE', #88745, 0.1000000000000028644 ) ;
#47161=DIRECTION ( 'NONE',  ( -1.000000000000000000, 0.000000000000000000, 0.000000000000000000 ) ) ;
#47333=CARTESIAN_POINT ( 'NONE',  ( 17.23472005113827876, 65.69211804551081002, -58.06968434459306394 ) ) ;
#48287=( BOUNDED_CURVE ( )  B_SPLINE_CURVE ( 3, ( #195342, #174529, #94916, #118356 ),
 .UNSPECIFIED., .F., .F. ) 
 B_SPLINE_CURVE_WITH_KNOTS ( ( 4, 4 ),
 ( 3.752122642744585068, 4.712388980384675463 ),
 .UNSPECIFIED. ) 
 CURVE ( )  GEOMETRIC_REPRESENTATION_ITEM ( )  RATIONAL_B_SPLINE_CURVE ( ( 1.000000000000000000, 0.9246222802177217481, 0.9246222802177217481, 1.000000000000000000 ) ) 
 REPRESENTATION_ITEM ( '' )  );
#48425=CARTESIAN_POINT ( 'NONE',  ( -23.25000000000000355, 64.25000000001161027, -60.27310748452440947 ) ) ;
#48473=ORIENTED_EDGE ( 'NONE', *, *, #10009, .F. ) ;
#48549=EDGE_CURVE ( 'NONE', #250894, #156714, #13233, .T. ) ;
#48726=ORIENTED_EDGE ( 'NONE', *, *, #252576, .T. ) ;
#48902=VERTEX_POINT ( 'NONE', #183840 ) ;
#49289=CARTESIAN_POINT ( 'NONE',  ( -16.94445028196807002, 66.00793639031378746, -48.63043766294283898 ) ) ;
#49426=LINE ( 'NONE', #91117, #150557 ) ;
#49453=DIRECTION ( 'NONE',  ( -0.000000000000000000, -6.982962677686266711E-15, 1.000000000000000000 ) ) ;
#49461=CARTESIAN_POINT ( 'NONE',  ( -16.87683809663752399, 66.05000000001157900, -56.87310748452438958 ) ) ;
#49493=EDGE_CURVE ( 'NONE', #253814, #65805, #141079, .T. ) ;
#49810=EDGE_CURVE ( 'NONE', #86511, #5771, #204037, .T. ) ;
#49921=CARTESIAN_POINT ( 'NONE',  ( -16.78805706634180339, 66.05174750694033037, -48.67895427649254003 ) ) ;
#49930=ORIENTED_EDGE ( 'NONE', *, *, #122078, .F. ) ;
#50005=EDGE_CURVE ( 'NONE', #111912, #13073, #76626, .T. ) ;
#50105=LINE ( 'NONE', #170112, #252459 ) ;
#50209=PLANE ( 'NONE',  #201635 ) ;
#50350=LINE ( 'NONE', #29566, #153702 ) ;
#50437=DIRECTION ( 'NONE',  ( 0.000000000000000000, 1.000000000000000000, 0.000000000000000000 ) ) ;
#50457=CARTESIAN_POINT ( 'NONE',  ( -15.75000000000000355, 66.65000000001155911, -52.77310748452439526 ) ) ;
#50550=CARTESIAN_POINT ( 'NONE',  ( -16.90128866880176162, 66.04620422280855507, -48.66043130113575188 ) ) ;
#50915=CIRCLE ( 'NONE', #5112, 1.500000000000001332 ) ;
#51149=EDGE_LOOP ( 'NONE', ( #175988, #97930, #49930, #154547 ) ) ;
#51497=ORIENTED_EDGE ( 'NONE', *, *, #159489, .T. ) ;
#51743=CARTESIAN_POINT ( 'NONE',  ( -15.57281606413133801, 66.62934494888806114, -51.99728422854350640 ) ) ;
#51835=CARTESIAN_POINT ( 'NONE',  ( -16.93415306273742260, 66.00437773999901481, -48.61305054216397536 ) ) ;
#51908=DIRECTION ( 'NONE',  ( -0.000000000000000000, -6.982962677686266711E-15, 1.000000000000000000 ) ) ;
#52019=CARTESIAN_POINT ( 'NONE',  ( -18.40000000000000213, 64.25000000001159606, -56.87310748452440379 ) ) ;
#52118=LINE ( 'NONE', #216336, #105087 ) ;
#52172=CARTESIAN_POINT ( 'NONE',  ( 18.39999999999999503, 70.35000000001153353, -48.67310748452436542 ) ) ;
#52194=CARTESIAN_POINT ( 'NONE',  ( -16.92989143108097849, 66.05000000001157900, -56.64062360976772226 ) ) ;
#52353=EDGE_CURVE ( 'NONE', #94765, #16521, #101354, .T. ) ;
#52365=CARTESIAN_POINT ( 'NONE',  ( -16.93255653858138388, 66.00154854603441379, -56.94146411653471773 ) ) ;
#52518=EDGE_CURVE ( 'NONE', #154587, #122321, #155010, .T. ) ;
#52600=CYLINDRICAL_SURFACE ( 'NONE', #238643, 0.1000000000000028644 ) ;
#52672=ORIENTED_EDGE ( 'NONE', *, *, #72927, .F. ) ;
#53194=EDGE_CURVE ( 'NONE', #160249, #16468, #57889, .T. ) ;
#53236=( BOUNDED_SURFACE ( )  B_SPLINE_SURFACE ( 3, 2, ( 
 ( #242910, #64283, #224626 ),
 ( #82524, #43438, #124268 ),
 ( #45993, #203786, #176866 ),
 ( #25178, #116868, #235518 ) ),
 .UNSPECIFIED., .F., .F., .F. ) 
 B_SPLINE_SURFACE_WITH_KNOTS ( ( 4, 4 ),
 ( 3, 3 ),
 ( 3.658908243880890421, 4.712388980384689674 ),
 ( 0.000000000000000000, 1.000000000000000000 ),
 .UNSPECIFIED. ) 
 GEOMETRIC_REPRESENTATION_ITEM ( )  RATIONAL_B_SPLINE_SURFACE ( (
 ( 1.000000000000000000, 0.8984936768950618768, 1.000000000000000000),
 ( 1.000000000000000000, 0.8646876308615185636, 1.000000000000000000),
 ( 1.000000000000000000, 0.7953136715913637911, 1.000000000000000000),
 ( 1.000000000000000000, 0.7071067811865475727, 1.000000000000000000) ) ) 
 REPRESENTATION_ITEM ( '' )  SURFACE ( )  );
#53237=VECTOR ( 'NONE', #184257, 1000.000000000000000 ) ;
#53292=FACE_OUTER_BOUND ( 'NONE', #102238, .T. ) ;
#53354=VERTEX_POINT ( 'NONE', #85138 ) ;
#53553=ORIENTED_EDGE ( 'NONE', *, *, #241499, .T. ) ;
#53856=ORIENTED_EDGE ( 'NONE', *, *, #90651, .F. ) ;
#53915=EDGE_CURVE ( 'NONE', #187671, #224622, #172990, .T. ) ;
#54094=CARTESIAN_POINT ( 'NONE',  ( -16.78569801330232281, 66.05206626689808047, -56.86619457917689147 ) ) ;
#54160=AXIS2_PLACEMENT_3D ( 'NONE', #255782, #38083, #56322 ) ;
#54405=ORIENTED_EDGE ( 'NONE', *, *, #30710, .F. ) ;
#54409=CARTESIAN_POINT ( 'NONE',  ( 15.75000000000000355, 66.65000000001157332, -53.00453852712175262 ) ) ;
#54420=ORIENTED_EDGE ( 'NONE', *, *, #34415, .F. ) ;
#54439=DIRECTION ( 'NONE',  ( -1.000000000000000000, 0.000000000000000000, -0.000000000000000000 ) ) ;
#54553=DIRECTION ( 'NONE',  ( 1.000000000000000000, -0.000000000000000000, 0.000000000000000000 ) ) ;
#54562=DIRECTION ( 'NONE',  ( -1.000000000000000000, 0.000000000000000000, 0.000000000000000000 ) ) ;
#54718=ORIENTED_EDGE ( 'NONE', *, *, #48549, .T. ) ;
#54820=EDGE_CURVE ( 'NONE', #122321, #254423, #134696, .T. ) ;
#54953=DIRECTION ( 'NONE',  ( 0.7071067811865463515, 0.7071067811865487940, 4.937700262164540154E-15 ) ) ;
#55011=FACE_OUTER_BOUND ( 'NONE', #164366, .T. ) ;
#55106=ADVANCED_FACE ( 'NONE', ( #173503 ), #32698, .F. ) ;
#55152=VECTOR ( 'NONE', #156836, 1000.000000000000000 ) ;
#55159=CARTESIAN_POINT ( 'NONE',  ( 13.22461703343584993, 66.56333706821246210, -51.20007075222952153 ) ) ;
#55247=VECTOR ( 'NONE', #168940, 1000.000000000000000 ) ;
#55432=ORIENTED_EDGE ( 'NONE', *, *, #165153, .F. ) ;
#55463=CIRCLE ( 'NONE', #222068, 0.9000000000000014655 ) ;
#55667=CARTESIAN_POINT ( 'NONE',  ( -16.93433913041102912, 65.99402157848757611, -48.58774205712922623 ) ) ;
#55669=CARTESIAN_POINT ( 'NONE',  ( -16.88495309932522659, 66.04537294153871585, -56.88855881071248177 ) ) ;
#55710=AXIS2_PLACEMENT_3D ( 'NONE', #151083, #89803, #209773 ) ;
#56317=DIRECTION ( 'NONE',  ( 0.000000000000000000, 1.000000000000000000, 6.982962677686266711E-15 ) ) ;
#56322=DIRECTION ( 'NONE',  ( 0.000000000000000000, -6.982962677686266711E-15, 1.000000000000000000 ) ) ;
#56340=( LENGTH_UNIT ( ) NAMED_UNIT ( * ) SI_UNIT ( .MILLI., .METRE. ) );
#56548=EDGE_CURVE ( 'NONE', #132612, #163978, #239052, .T. ) ;
#56694=CARTESIAN_POINT ( 'NONE',  ( -16.87683809663752399, 66.15000000001157332, -56.12074346632808641 ) ) ;
#56969=DIRECTION ( 'NONE',  ( -1.000000000000000000, 0.000000000000000000, -0.000000000000000000 ) ) ;
#57107=DIRECTION ( 'NONE',  ( -0.000000000000000000, -6.982962677686266711E-15, 1.000000000000000000 ) ) ;
#57210=DIRECTION ( 'NONE',  ( -0.000000000000000000, -6.982962677686266711E-15, 1.000000000000000000 ) ) ;
#57410=VERTEX_POINT ( 'NONE', #22941 ) ;
#57607=DIRECTION ( 'NONE',  ( -0.7071067811865301422, 0.7071067811865648922, 0.000000000000000000 ) ) ;
#57715=B_SPLINE_CURVE_WITH_KNOTS ( 'NONE', 3,
 ( #10805, #12110, #150327, #129469, #206430, #49921, #207736, #146435, #68209, #91623 ),
 .UNSPECIFIED., .F., .F.,
 ( 4, 3, 3, 4 ),
 ( -2.000561356209491534E-06, 0.000000000000000000, 1.787822682428948123E-05, 4.206475347090216207E-05 ),
 .UNSPECIFIED. ) ;
#57749=CARTESIAN_POINT ( 'NONE',  ( 12.60873083341396139, 66.61042836546511126, -51.70546677215522635 ) ) ;
#57780=CARTESIAN_POINT ( 'NONE',  ( 23.04999999999999716, 67.17743825834517679, -56.87310748452437537 ) ) ;
#57865=CARTESIAN_POINT ( 'NONE',  ( -15.75000000000000355, 66.15000000001155911, -52.77310748452439526 ) ) ;
#57889=LINE ( 'NONE', #253529, #63045 ) ;
#57953=CARTESIAN_POINT ( 'NONE',  ( -17.11825945287481332, 65.95000000001152785, -48.77310748452439526 ) ) ;
#58043=ORIENTED_EDGE ( 'NONE', *, *, #132402, .F. ) ;
#58072=VECTOR ( 'NONE', #89971, 1000.000000000000000 ) ;
#58116=CARTESIAN_POINT ( 'NONE',  ( -16.94309007106720344, 66.00777380744158052, -56.91731620196888741 ) ) ;
#58568=CARTESIAN_POINT ( 'NONE',  ( -16.87683809663752044, 66.05000000001153637, -49.42547150272070411 ) ) ;
#58943=CARTESIAN_POINT ( 'NONE',  ( 20.09999999999999787, 66.25000000001156764, -48.67310748452440095 ) ) ;
#59000=CARTESIAN_POINT ( 'NONE',  ( -20.65000000000000568, 68.75000000001161027, -60.27310748452437394 ) ) ;
#59024=ORIENTED_EDGE ( 'NONE', *, *, #52353, .T. ) ;
#59100=CARTESIAN_POINT ( 'NONE',  ( -17.11825945287482753, 65.95000000001159890, -56.87310748452438958 ) ) ;
#59134=AXIS2_PLACEMENT_3D ( 'NONE', #179321, #222245, #201419 ) ;
#59185=ADVANCED_FACE ( 'NONE', ( #197124 ), #40676, .F. ) ;
#59240=FACE_BOUND ( 'NONE', #107613, .T. ) ;
#59309=ADVANCED_FACE ( 'NONE', ( #156757 ), #236259, .F. ) ;
#59367=DIRECTION ( 'NONE',  ( -0.000000000000000000, -6.982962677686266711E-15, 1.000000000000000000 ) ) ;
#59434=DIRECTION ( 'NONE',  ( 1.000000000000000000, 0.000000000000000000, 0.000000000000000000 ) ) ;
#59502=DIRECTION ( 'NONE',  ( 0.2834754621636358940, 0.2834754621636501049, -0.9161240771326873977 ) ) ;
#59845=CARTESIAN_POINT ( 'NONE',  ( -16.97683809663752186, 66.05000000001153637, -49.42547150272071121 ) ) ;
#59941=ORIENTED_EDGE ( 'NONE', *, *, #42695, .T. ) ;
#60244=CARTESIAN_POINT ( 'NONE',  ( -16.87372386987899375, 66.11939976637481209, -56.37383761265798654 ) ) ;
#60432=DIRECTION ( 'NONE',  ( -0.000000000000000000, -6.982962677686266711E-15, 1.000000000000000000 ) ) ;
#60530=LINE ( 'NONE', #120545, #76263 ) ;
#60601=EDGE_CURVE ( 'NONE', #202498, #37588, #7362, .T. ) ;
#60663=CARTESIAN_POINT ( 'NONE',  ( -13.88555196119803625, 66.54256847116265305, -54.52319054662474684 ) ) ;
#60776=ORIENTED_EDGE ( 'NONE', *, *, #6505, .T. ) ;
#60813=CARTESIAN_POINT ( 'NONE',  ( -16.93658623642902583, 66.01961832835444000, -56.91120475539518964 ) ) ;
#60836=PLANE ( 'NONE',  #196722 ) ;
#61137=ADVANCED_FACE ( 'NONE', ( #125116 ), #205912, .F. ) ;
#61291=CARTESIAN_POINT ( 'NONE',  ( -16.87036670365548474, 66.01058118070987746, -48.54354736722234520 ) ) ;
#61297=VECTOR ( 'NONE', #149308, 999.9999999999998863 ) ;
#61559=CARTESIAN_POINT ( 'NONE',  ( -16.96982749440684657, 66.05000000001157900, -56.39832907571204146 ) ) ;
#61902=CARTESIAN_POINT ( 'NONE',  ( -16.86445178670626888, 66.03778837089552667, -56.91388492264187704 ) ) ;
#61974=CARTESIAN_POINT ( 'NONE',  ( -14.45443560709636266, 66.54940788787786232, -54.46691916571599990 ) ) ;
#61977=EDGE_CURVE ( 'NONE', #209103, #46675, #142899, .T. ) ;
#62127=PLANE ( 'NONE',  #155327 ) ;
#62256=ORIENTED_EDGE ( 'NONE', *, *, #173338, .F. ) ;
#62320=ORIENTED_EDGE ( 'NONE', *, *, #104652, .F. ) ;
#62590=EDGE_LOOP ( 'NONE', ( #24568, #240254, #237496, #99875 ) ) ;
#62715=ORIENTED_EDGE ( 'NONE', *, *, #252576, .F. ) ;
#62749=FACE_OUTER_BOUND ( 'NONE', #230472, .T. ) ;
#62916=CARTESIAN_POINT ( 'NONE',  ( -12.25000000000000178, 66.65000000001155911, -52.77310748452439526 ) ) ;
#63045=VECTOR ( 'NONE', #136130, 999.9999999999998863 ) ;
#63286=CARTESIAN_POINT ( 'NONE',  ( -23.25000000000000355, 70.35000000001159037, -56.87310748452436115 ) ) ;
#63300=EDGE_LOOP ( 'NONE', ( #234871, #80354, #144881, #111521, #65987, #106389 ) ) ;
#63364=VERTEX_POINT ( 'NONE', #28018 ) ;
#63961=ORIENTED_EDGE ( 'NONE', *, *, #10479, .T. ) ;
#63977=CARTESIAN_POINT ( 'NONE',  ( 20.73486653747088582, 68.75000000001156764, -60.27310748452437394 ) ) ;
#63985=ORIENTED_EDGE ( 'NONE', *, *, #70424, .F. ) ;
#64283=CARTESIAN_POINT ( 'NONE',  ( -16.91049119928362998, 66.05000000001153637, -48.64138709133355576 ) ) ;
#64317=CARTESIAN_POINT ( 'NONE',  ( 18.39999999999999503, 64.25000000001159606, -56.87310748452440379 ) ) ;
#64401=EDGE_CURVE ( 'NONE', #239112, #180347, #177001, .T. ) ;
#64476=CARTESIAN_POINT ( 'NONE',  ( -16.85718274719441823, 66.02385768538987065, -56.95976115234177684 ) ) ;
#64568=VECTOR ( 'NONE', #37802, 1000.000000000000000 ) ;
#64592=DIRECTION ( 'NONE',  ( -1.186688945009010077E-16, -1.000000000000000000, -6.789366196018717631E-15 ) ) ;
#64756=ADVANCED_FACE ( 'NONE', ( #88670 ), #225610, .T. ) ;
#64762=DIRECTION ( 'NONE',  ( 1.186688945009010077E-16, 1.000000000000000000, 6.982962677686266711E-15 ) ) ;
#64840=CARTESIAN_POINT ( 'NONE',  ( -16.81744102076748959, 66.05000000001153637, -48.67310748452439384 ) ) ;
#64908=CARTESIAN_POINT ( 'NONE',  ( -17.29838795458362100, 65.62845014206548910, -58.12784876713939752 ) ) ;
#65000=CARTESIAN_POINT ( 'NONE',  ( -16.84981964351508665, 66.08268176591256804, -48.89270909854381131 ) ) ;
#65032=( BOUNDED_SURFACE ( )  B_SPLINE_SURFACE ( 3, 2, ( 
 ( #122988, #182964, #224631 ),
 ( #126826, #105950, #164675 ),
 ( #8173, #86378, #163393 ),
 ( #124271, #223340, #65561 ) ),
 .UNSPECIFIED., .F., .F., .F. ) 
 B_SPLINE_SURFACE_WITH_KNOTS ( ( 4, 4 ),
 ( 3, 3 ),
 ( 0.0008258556059633768206, 0.0009616864997632841496 ),
 ( 0.000000000000000000, 1.000000000000000000 ),
 .UNSPECIFIED. ) 
 GEOMETRIC_REPRESENTATION_ITEM ( )  RATIONAL_B_SPLINE_SURFACE ( (
 ( 1.000000000000000000, 0.9152888060719408525, 1.000000000000000000),
 ( 1.000000000000000000, 0.9327727094138220654, 1.000000000000000000),
 ( 1.000000000000000000, 0.9369023509258298521, 1.000000000000000000),
 ( 1.000000000000000000, 0.9246339933864542449, 1.000000000000000000) ) ) 
 REPRESENTATION_ITEM ( '' )  SURFACE ( )  );
#65197=DIRECTION ( 'NONE',  ( 1.000000000000000000, -1.646408749285562060E-14, -1.073024830501232702E-15 ) ) ;
#65295=ORIENTED_EDGE ( 'NONE', *, *, #219145, .T. ) ;
#65390=CARTESIAN_POINT ( 'NONE',  ( -16.85312841634287295, 66.08639382269134899, -56.62593435123186936 ) ) ;
#65559=FACE_OUTER_BOUND ( 'NONE', #244813, .T. ) ;
#65561=CARTESIAN_POINT ( 'NONE',  ( -16.94878442675511110, 66.00827089702052319, -48.63488790888651891 ) ) ;
#65573=ORIENTED_EDGE ( 'NONE', *, *, #15520, .F. ) ;
#65596=LINE ( 'NONE', #64317, #53237 ) ;
#65805=VERTEX_POINT ( 'NONE', #137460 ) ;
#65905=CARTESIAN_POINT ( 'NONE',  ( 20.73486653747088937, 68.25000000001149658, -48.67310748452437963 ) ) ;
#65950=ORIENTED_EDGE ( 'NONE', *, *, #18185, .F. ) ;
#65987=ORIENTED_EDGE ( 'NONE', *, *, #92267, .F. ) ;
#66001=VECTOR ( 'NONE', #60432, 1000.000000000000000 ) ;
#66132=CARTESIAN_POINT ( 'NONE',  ( -16.90138253750127362, 66.05000000001155058, -48.81154477661981161 ) ) ;
#66219=ORIENTED_EDGE ( 'NONE', *, *, #130200, .T. ) ;
#66258=ORIENTED_EDGE ( 'NONE', *, *, #42695, .F. ) ;
#66291=EDGE_LOOP ( 'NONE', ( #220439, #102435, #99722, #63961, #172145, #245806 ) ) ;
#66343=DIRECTION ( 'NONE',  ( -1.000000000000000000, 0.000000000000000000, -0.000000000000000000 ) ) ;
#66419=ORIENTED_EDGE ( 'NONE', *, *, #49810, .F. ) ;
#66470=PLANE ( 'NONE',  #115610 ) ;
#66830=CARTESIAN_POINT ( 'NONE',  ( 12.25000000000000000, 66.65000000001155911, -52.77310748452440237 ) ) ;
#66931=ORIENTED_EDGE ( 'NONE', *, *, #49493, .T. ) ;
#67039=CARTESIAN_POINT ( 'NONE',  ( -16.90202395485742670, 66.03405545546095823, -56.92612120578434087 ) ) ;
#67573=CARTESIAN_POINT ( 'NONE',  ( -16.88783316861814754, 66.05000000001153637, -48.77537152650415919 ) ) ;
#67665=ORIENTED_EDGE ( 'NONE', *, *, #3424, .T. ) ;
#67688=CIRCLE ( 'NONE', #180138, 0.9000000000000014655 ) ;
#67739=DIRECTION ( 'NONE',  ( 0.000000000000000000, 6.982962677686266711E-15, -1.000000000000000000 ) ) ;
#67813=ORIENTED_EDGE ( 'NONE', *, *, #44947, .F. ) ;
#67819=VECTOR ( 'NONE', #123669, 1000.000000000000000 ) ;
#67889=LINE ( 'NONE', #70498, #227910 ) ;
#68080=CARTESIAN_POINT ( 'NONE',  ( -16.88005004766534967, 66.04989949669047178, -48.67277137257563879 ) ) ;
#68128=CARTESIAN_POINT ( 'NONE',  ( -15.55912972643741199, 67.50912972644901799, -56.97310748452438389 ) ) ;
#68184=CARTESIAN_POINT ( 'NONE',  ( 21.13736287352038445, 67.95335762362751097, -48.67310748452438673 ) ) ;
#68209=CARTESIAN_POINT ( 'NONE',  ( -16.80939487329394666, 66.05000000001153637, -48.67310748452351277 ) ) ;
#68330=CARTESIAN_POINT ( 'NONE',  ( -16.86379686415369150, 66.02478224075835556, -48.58971759543411650 ) ) ;
#68337=B_SPLINE_CURVE_WITH_KNOTS ( 'NONE', 3,
 ( #198088, #76851, #37759, #175987, #218923, #254195, #1151, #156437, #215087, #118576, #19464, #36481, #235924, #138099 ),
 .UNSPECIFIED., .F., .F.,
 ( 4, 2, 2, 2, 2, 2, 4 ),
 ( 1.387778780781445676E-17, 0.0003823333598417824023, 0.0005735000397626774252, 0.0006690833797231165612, 0.0007168750497033334187, 0.0007407708846934392454, 0.0007646667196835449636 ),
 .UNSPECIFIED. ) ;
#68580=VERTEX_POINT ( 'NONE', #191532 ) ;
#68754=ORIENTED_EDGE ( 'NONE', *, *, #168901, .T. ) ;
#68910=ADVANCED_FACE ( 'NONE', ( #23154 ), #86924, .F. ) ;
#68935=AXIS2_PLACEMENT_3D ( 'NONE', #21498, #44900, #203960 ) ;
#68996=CARTESIAN_POINT ( 'NONE',  ( -18.35663730107557257, 64.52609257350039229, -60.27310748452440947 ) ) ;
#69144=CARTESIAN_POINT ( 'NONE',  ( -18.39418127959864790, 64.51609439831335635, -45.27310748452440947 ) ) ;
#69191=ORIENTED_EDGE ( 'NONE', *, *, #45885, .F. ) ;
#69912=CARTESIAN_POINT ( 'NONE',  ( -16.87331047859651179, 66.05000000001157900, -56.87310748452438958 ) ) ;
#70012=CARTESIAN_POINT ( 'NONE',  ( -16.97048361161166596, 66.05000000001150795, -49.16422314009399486 ) ) ;
#70023=ORIENTED_EDGE ( 'NONE', *, *, #225698, .T. ) ;
#70171=CARTESIAN_POINT ( 'NONE',  ( -16.89268316805465986, 66.04827818676933759, -48.66735500597884823 ) ) ;
#70243=DIRECTION ( 'NONE',  ( 0.000000000000000000, -1.000000000000000000, -6.982962677686266711E-15 ) ) ;
#70354=DIRECTION ( 'NONE',  ( 0.000000000000000000, -6.982962677686266711E-15, 1.000000000000000000 ) ) ;
#70361=FACE_OUTER_BOUND ( 'NONE', #82152, .T. ) ;
#70404=AXIS2_PLACEMENT_3D ( 'NONE', #171930, #149781, #72818 ) ;
#70424=EDGE_CURVE ( 'NONE', #101287, #12212, #221044, .T. ) ;
#70498=CARTESIAN_POINT ( 'NONE',  ( 18.39999999999999503, 64.25000000001159606, -56.87310748452440379 ) ) ;
#70530=CARTESIAN_POINT ( 'NONE',  ( -17.04295772865462411, 65.97510057475010115, -56.87310748452439668 ) ) ;
#70812=ORIENTED_EDGE ( 'NONE', *, *, #201933, .T. ) ;
#70966=CARTESIAN_POINT ( 'NONE',  ( 18.39999999999997371, 64.52683809664901560, -45.27310748452439526 ) ) ;
#71110=VERTEX_POINT ( 'NONE', #243509 ) ;
#71182=VECTOR ( 'NONE', #214752, 1000.000000000000000 ) ;
#71190=CARTESIAN_POINT ( 'NONE',  ( -17.01473183483382101, 66.05000000001157900, -56.77310748452439526 ) ) ;
#71430=CARTESIAN_POINT ( 'NONE',  ( 12.84233041328156588, 66.58946139148270049, -54.09041948738352090 ) ) ;
#71440=DIRECTION ( 'NONE',  ( -1.073024830501117725E-15, 6.982962677686266711E-15, -1.000000000000000000 ) ) ;
#71462=ORIENTED_EDGE ( 'NONE', *, *, #226015, .T. ) ;
#71687=ADVANCED_FACE ( 'NONE', ( #147962 ), #110110, .T. ) ;
#72063=DIRECTION ( 'NONE',  ( -1.000000000000000000, 0.000000000000000000, 0.000000000000000000 ) ) ;
#72185=VECTOR ( 'NONE', #162065, 1000.000000000000000 ) ;
#72232=PLANE ( 'NONE',  #43652 ) ;
#72301=VECTOR ( 'NONE', #162499, 1000.000000000000000 ) ;
#72334=CARTESIAN_POINT ( 'NONE',  ( -16.94107738177415712, 65.98576071487495653, -56.97310748452439810 ) ) ;
#72404=CARTESIAN_POINT ( 'NONE',  ( -16.79184697841823493, 66.05123833835317271, -56.86896521392187509 ) ) ;
#72441=ORIENTED_EDGE ( 'NONE', *, *, #7601, .F. ) ;
#72594=DIRECTION ( 'NONE',  ( 0.000000000000000000, -6.982962677686266711E-15, 1.000000000000000000 ) ) ;
#72642=CARTESIAN_POINT ( 'NONE',  ( -14.11361717019515893, 66.54257354752263609, -51.02306561612434876 ) ) ;
#72687=VECTOR ( 'NONE', #231986, 1000.000000000000000 ) ;
#72690=ORIENTED_EDGE ( 'NONE', *, *, #88758, .F. ) ;
#72745=CARTESIAN_POINT ( 'NONE',  ( -16.93935632781549572, 66.01526950028642204, -48.63344673581409694 ) ) ;
#72818=DIRECTION ( 'NONE',  ( 0.000000000000000000, -0.9553114395362733990, 0.2956011730205631016 ) ) ;
#72833=EDGE_CURVE ( 'NONE', #213752, #120974, #213104, .T. ) ;
#72860=EDGE_CURVE ( 'NONE', #146300, #63364, #73087, .T. ) ;
#72893=DIRECTION ( 'NONE',  ( -1.020425574104004196E-15, 6.982962677686266711E-15, -1.000000000000000000 ) ) ;
#72927=EDGE_CURVE ( 'NONE', #206343, #230076, #115291, .T. ) ;
#72986=EDGE_CURVE ( 'NONE', #254423, #100756, #202753, .T. ) ;
#73013=LINE ( 'NONE', #244204, #215350 ) ;
#73087=( BOUNDED_CURVE ( )  B_SPLINE_CURVE ( 3, ( #72334, #132284, #33232, #192279 ),
 .UNSPECIFIED., .F., .F. ) 
 B_SPLINE_CURVE_WITH_KNOTS ( ( 4, 4 ),
 ( 0.3000847527772380618, 0.5497968875596825900 ),
 .UNSPECIFIED. ) 
 CURVE ( )  GEOMETRIC_REPRESENTATION_ITEM ( )  RATIONAL_B_SPLINE_CURVE ( ( 1.000000000000000000, 0.9948104011409419911, 0.9948104011409419911, 1.000000000000000000 ) ) 
 REPRESENTATION_ITEM ( '' )  );
#73123=DIRECTION ( 'NONE',  ( 1.000000000000000000, 0.000000000000000000, 0.000000000000000000 ) ) ;
#73270=CARTESIAN_POINT ( 'NONE',  ( -16.93226657140833069, 66.00045617728716252, -56.94439437355077871 ) ) ;
#73679=ORIENTED_EDGE ( 'NONE', *, *, #103315, .F. ) ;
#73909=DIRECTION ( 'NONE',  ( -0.000000000000000000, -6.982962677686266711E-15, 1.000000000000000000 ) ) ;
#73925=PRODUCT_DEFINITION_FORMATION_WITH_SPECIFIED_SOURCE ( 'ANY', '', #86733, .NOT_KNOWN. ) ;
#73934=CARTESIAN_POINT ( 'NONE',  ( -13.11924609551134857, 66.56831044948742715, -51.24381745228831875 ) ) ;
#74014=ORIENTED_EDGE ( 'NONE', *, *, #243846, .T. ) ;
#74016=CARTESIAN_POINT ( 'NONE',  ( 15.70340296795548163, 66.64411154550899141, -53.23446458774640178 ) ) ;
#74058=EDGE_CURVE ( 'NONE', #37588, #101180, #2956, .T. ) ;
#74071=DIRECTION ( 'NONE',  ( 0.000000000000000000, -1.000000000000000000, -6.982962677686266711E-15 ) ) ;
#74304=DIRECTION ( 'NONE',  ( 0.000000000000000000, -1.000000000000000000, -6.982962677686266711E-15 ) ) ;
#74806=CARTESIAN_POINT ( 'NONE',  ( 13.54577453029515510, 66.54939790392303678, -51.07921152142773735 ) ) ;
#75063=CARTESIAN_POINT ( 'NONE',  ( -16.27683809663750480, 66.65000000001153069, -48.57310748452439242 ) ) ;
#75168=FACE_OUTER_BOUND ( 'NONE', #235537, .T. ) ;
#75590=EDGE_CURVE ( 'NONE', #53354, #213752, #4295, .T. ) ;
#75716=CIRCLE ( 'NONE', #38297, 0.1999999999999987899 ) ;
#75883=CARTESIAN_POINT ( 'NONE',  ( 13.99999999999999822, 66.15000000001155911, -52.77310748452440237 ) ) ;
#76127=ORIENTED_EDGE ( 'NONE', *, *, #222519, .T. ) ;
#76263=VECTOR ( 'NONE', #201339, 1000.000000000000000 ) ;
#76479=ORIENTED_EDGE ( 'NONE', *, *, #196603, .T. ) ;
#76576=EDGE_CURVE ( 'NONE', #71110, #99076, #12642, .T. ) ;
#76580=EDGE_LOOP ( 'NONE', ( #36659, #108095, #117643, #96824 ) ) ;
#76626=LINE ( 'NONE', #132779, #203638 ) ;
#76657=ORIENTED_EDGE ( 'NONE', *, *, #50005, .F. ) ;
#76851=CARTESIAN_POINT ( 'NONE',  ( -16.87683809663752399, 66.13508655273133741, -49.29882593322043505 ) ) ;
#76925=SURFACE_STYLE_USAGE ( .BOTH. , #16979 ) ;
#76969=VERTEX_POINT ( 'NONE', #108839 ) ;
#77085=VECTOR ( 'NONE', #57210, 1000.000000000000000 ) ;
#77314=CARTESIAN_POINT ( 'NONE',  ( 15.31784899511109899, 66.60336962369380842, -51.61605009170609293 ) ) ;
#77568=CARTESIAN_POINT ( 'NONE',  ( 20.05000000000002913, 68.75000000001155342, -56.87310748452436826 ) ) ;
#77591=( GEOMETRIC_REPRESENTATION_CONTEXT ( 3 ) GLOBAL_UNCERTAINTY_ASSIGNED_CONTEXT ( ( #175790 ) ) GLOBAL_UNIT_ASSIGNED_CONTEXT ( ( #56340, #94189, #116351 ) ) REPRESENTATION_CONTEXT ( 'NONE', 'WORKASPACE' ) );
#77681=PLANE ( 'NONE',  #197034 ) ;
#77842=EDGE_CURVE ( 'NONE', #208794, #156714, #150466, .T. ) ;
#78135=FACE_OUTER_BOUND ( 'NONE', #243924, .T. ) ;
#78142=ORIENTED_EDGE ( 'NONE', *, *, #38179, .F. ) ;
#78170=VERTEX_POINT ( 'NONE', #218246 ) ;
#78352=ORIENTED_EDGE ( 'NONE', *, *, #188332, .F. ) ;
#78601=CARTESIAN_POINT ( 'NONE',  ( 12.42718393586865844, 66.62934494888806114, -51.99728422854352772 ) ) ;
#78832=DIRECTION ( 'NONE',  ( -1.000000000000000000, 1.646408749285563322E-14, -1.073024830501002749E-15 ) ) ;
#78930=CARTESIAN_POINT ( 'NONE',  ( -13.22483237240078857, 66.56332574816870817, -54.34624555352518627 ) ) ;
#78952=DIRECTION ( 'NONE',  ( 1.000000000000000000, -1.186688945009010077E-16, -8.286604613020808509E-31 ) ) ;
#78956=LINE ( 'NONE', #158551, #88698 ) ;
#78983=AXIS2_PLACEMENT_3D ( 'NONE', #126889, #248110, #72063 ) ;
#79257=CARTESIAN_POINT ( 'NONE',  ( -33.72168855820451938, 66.05000000001152216, -48.67310748452433700 ) ) ;
#79314=ORIENTED_EDGE ( 'NONE', *, *, #222519, .F. ) ;
#79948=ADVANCED_FACE ( 'NONE', ( #213856 ), #153936, .F. ) ;
#79987=EDGE_CURVE ( 'NONE', #105113, #197047, #189051, .T. ) ;
#80095=DIRECTION ( 'NONE',  ( 0.000000000000000000, -6.789366196018718420E-15, 1.000000000000000000 ) ) ;
#80159=EDGE_LOOP ( 'NONE', ( #207516, #183139, #222579 ) ) ;
#80179=CARTESIAN_POINT ( 'NONE',  ( -21.64999999999999858, 65.95000000001152785, -48.77310748452439526 ) ) ;
#80194=EDGE_CURVE ( 'NONE', #1286, #148974, #28543, .T. ) ;
#80319=CARTESIAN_POINT ( 'NONE',  ( 20.09999999999999787, 66.25000000001162448, -60.27310748452439526 ) ) ;
#80349=DIRECTION ( 'NONE',  ( 0.000000000000000000, 0.9553114395362733990, 0.2956011730205631016 ) ) ;
#80354=ORIENTED_EDGE ( 'NONE', *, *, #14243, .T. ) ;
#80433=LINE ( 'NONE', #180871, #150658 ) ;
#81098=CARTESIAN_POINT ( 'NONE',  ( -16.87998658237755123, 66.05000000001159322, -56.65946791678611305 ) ) ;
#81220=ORIENTED_EDGE ( 'NONE', *, *, #225698, .F. ) ;
#81418=CARTESIAN_POINT ( 'NONE',  ( -17.01473183483380325, 66.05000000001153637, -48.77310748452438816 ) ) ;
#81427=CARTESIAN_POINT ( 'NONE',  ( -16.87036670365549895, 66.01058118070992009, -57.00266760182645243 ) ) ;
#81494=CARTESIAN_POINT ( 'NONE',  ( -15.52965525596987817, 66.62446189796352769, -53.65323160353355547 ) ) ;
#81515=CARTESIAN_POINT ( 'NONE',  ( -16.77683809663752257, 52.34166666667822199, -52.77310748452448763 ) ) ;
#81521=CARTESIAN_POINT ( 'NONE',  ( -16.93909480342659890, 66.00692163521003408, -56.92276046785206489 ) ) ;
#81652=CARTESIAN_POINT ( 'NONE',  ( -16.93860193097148326, 66.00689223268226158, -48.62296911721753645 ) ) ;
#81677=COLOUR_RGB ( '', 0.08235294, 0.09019608, 0.10196078) ;
#81799=EDGE_LOOP ( 'NONE', ( #165650, #171674, #3627, #73679, #66419 ) ) ;
#81885=ORIENTED_EDGE ( 'NONE', *, *, #91262, .T. ) ;
#82094=DIRECTION ( 'NONE',  ( 1.186688945009009831E-16, 1.000000000000000000, 6.982962677686266711E-15 ) ) ;
#82152=EDGE_LOOP ( 'NONE', ( #146475, #36918, #250890, #243342, #144771, #35073, #51497, #193491, #140968 ) ) ;
#82162=FACE_OUTER_BOUND ( 'NONE', #66291, .T. ) ;
#82429=CYLINDRICAL_SURFACE ( 'NONE', #189149, 0.9000000000000014655 ) ;
#82524=CARTESIAN_POINT ( 'NONE',  ( -16.92209698673592300, 66.05000000001153637, -48.73374305157589959 ) ) ;
#82542=CARTESIAN_POINT ( 'NONE',  ( 18.54999999999999716, 67.25000000001156764, -60.27310748452438816 ) ) ;
#82549=DIRECTION ( 'NONE',  ( -1.000000000000000000, 1.186688945009010077E-16, 8.286604613020808509E-31 ) ) ;
#82588=CARTESIAN_POINT ( 'NONE',  ( 16.87683809663750267, 66.05000000001157900, -56.87310748452439668 ) ) ;
#83256=CARTESIAN_POINT ( 'NONE',  ( -16.87998658237717109, 66.05000000001153637, -48.88674705226281958 ) ) ;
#83295=CARTESIAN_POINT ( 'NONE',  ( -20.65000000000000568, 70.35000000001160458, -60.27310748452436684 ) ) ;
#83420=DIRECTION ( 'NONE',  ( 1.186688945009010077E-16, 1.000000000000000000, 6.982962677686266711E-15 ) ) ;
#83446=PLANE ( 'NONE',  #251528 ) ;
#83570=ORIENTED_EDGE ( 'NONE', *, *, #52353, .F. ) ;
#83593=CARTESIAN_POINT ( 'NONE',  ( -16.97683809663752186, 66.15000000001153069, -49.42547150272071121 ) ) ;
#83807=ORIENTED_EDGE ( 'NONE', *, *, #134142, .F. ) ;
#84162=ORIENTED_EDGE ( 'NONE', *, *, #60601, .T. ) ;
#84309=CARTESIAN_POINT ( 'NONE',  ( 18.39999999999999503, 64.25000000001153921, -48.67310748452440805 ) ) ;
#84519=CARTESIAN_POINT ( 'NONE',  ( -16.88705144915408596, 66.05000000001153637, -48.95408607923688038 ) ) ;
#84558=LINE ( 'NONE', #83295, #214610 ) ;
#84607=CARTESIAN_POINT ( 'NONE',  ( 23.24999999999999645, 70.35000000001159037, -56.87310748452435405 ) ) ;
#84694=CARTESIAN_POINT ( 'NONE',  ( 13.99999999999999822, 66.15000000001155911, -52.77310748452440237 ) ) ;
#84928=CARTESIAN_POINT ( 'NONE',  ( -16.82055514392384410, 66.05000000001159322, -56.84630940998236781 ) ) ;
#84975=VERTEX_POINT ( 'NONE', #164189 ) ;
#84998=DIRECTION ( 'NONE',  ( -0.000000000000000000, -6.982962677686266711E-15, 1.000000000000000000 ) ) ;
#85138=CARTESIAN_POINT ( 'NONE',  ( 23.24999999999999645, 67.17743825834517679, -56.87310748452437537 ) ) ;
#85312=EDGE_CURVE ( 'NONE', #245959, #209103, #80433, .T. ) ;
#85423=EDGE_LOOP ( 'NONE', ( #222007, #174959, #78142, #256784 ) ) ;
#85525=AXIS2_PLACEMENT_3D ( 'NONE', #223065, #126546, #44453 ) ;
#85570=CARTESIAN_POINT ( 'NONE',  ( -18.40000000000000213, 64.52683809664954140, -45.32293673299014358 ) ) ;
#85859=AXIS2_PLACEMENT_3D ( 'NONE', #33164, #112665, #113933 ) ;
#85883=DIRECTION ( 'NONE',  ( -1.000000000000000000, 0.000000000000000000, 0.000000000000000000 ) ) ;
#85935=DIRECTION ( 'NONE',  ( 0.000000000000000000, 6.982962677686266711E-15, -1.000000000000000000 ) ) ;
#85936=DIRECTION ( 'NONE',  ( -1.000000000000000000, 0.000000000000000000, -0.000000000000000000 ) ) ;
#85984=ORIENTED_EDGE ( 'NONE', *, *, #257844, .T. ) ;
#86335=FACE_OUTER_BOUND ( 'NONE', #104571, .T. ) ;
#86378=CARTESIAN_POINT ( 'NONE',  ( -16.90202395485795250, 66.03405545546092981, -48.62009376326439991 ) ) ;
#86431=DIRECTION ( 'NONE',  ( -0.000000000000000000, -6.982962677686266711E-15, 1.000000000000000000 ) ) ;
#86511=VERTEX_POINT ( 'NONE', #126213 ) ;
#86729=EDGE_CURVE ( 'NONE', #16521, #241094, #213456, .T. ) ;
#86733=PRODUCT ( 'Snap Open Cable Crossbars 15', 'Snap Open Cable Crossbars 15', '', ( #252986 ) ) ;
#86924=PLANE ( 'NONE',  #129016 ) ;
#86989=ADVANCED_FACE ( 'NONE', ( #227575 ), #50209, .F. ) ;
#87020=CARTESIAN_POINT ( 'NONE',  ( -12.92414019175885898, 66.58236703690523939, -51.37415901879212754 ) ) ;
#87177=ORIENTED_EDGE ( 'NONE', *, *, #128898, .F. ) ;
#87400=EDGE_LOOP ( 'NONE', ( #11128, #39157, #85984, #253916 ) ) ;
#87643=CARTESIAN_POINT ( 'NONE',  ( -16.94037747912386394, 65.98646061752525327, -56.97197652654890021 ) ) ;
#87760=EDGE_LOOP ( 'NONE', ( #62320, #81220, #55432, #18981, #150018, #15614, #227539, #44282, #204434, #250554, #198993, #27424, #117096, #237474 ) ) ;
#87764=ORIENTED_EDGE ( 'NONE', *, *, #1364, .T. ) ;
#88296=CARTESIAN_POINT ( 'NONE',  ( -13.54036565897075306, 66.54845833862601978, -51.06923198569381128 ) ) ;
#88324=ORIENTED_EDGE ( 'NONE', *, *, #44947, .T. ) ;
#88602=CARTESIAN_POINT ( 'NONE',  ( 18.39999999999997371, 64.25000000001161027, -60.27310748452440947 ) ) ;
#88670=FACE_OUTER_BOUND ( 'NONE', #94841, .T. ) ;
#88698=VECTOR ( 'NONE', #198927, 1000.000000000000000 ) ;
#88745=AXIS2_PLACEMENT_3D ( 'NONE', #57953, #137490, #117941 ) ;
#88758=EDGE_CURVE ( 'NONE', #100756, #254423, #177652, .T. ) ;
#89456=VERTEX_POINT ( 'NONE', #21807 ) ;
#89803=DIRECTION ( 'NONE',  ( -1.073024830501117725E-15, -6.982962677686266711E-15, 1.000000000000000000 ) ) ;
#89915=CARTESIAN_POINT ( 'NONE',  ( -17.71734398241073905, 65.15764277154701745, -59.24824573752999157 ) ) ;
#89942=EDGE_CURVE ( 'NONE', #57410, #45783, #91421, .T. ) ;
#89971=DIRECTION ( 'NONE',  ( 1.000000000000000000, 0.000000000000000000, 0.000000000000000000 ) ) ;
#90231=DIRECTION ( 'NONE',  ( 0.7071067811865214825, -0.7071067811865735520, 0.000000000000000000 ) ) ;
#90236=VERTEX_POINT ( 'NONE', #222899 ) ;
#90318=AXIS2_PLACEMENT_3D ( 'NONE', #1746, #82549, #242935 ) ;
#90326=ADVANCED_FACE ( 'NONE', ( #31173 ), #149815, .F. ) ;
#90437=FACE_OUTER_BOUND ( 'NONE', #210044, .T. ) ;
#90651=EDGE_CURVE ( 'NONE', #162196, #13073, #183480, .T. ) ;
#90740=CARTESIAN_POINT ( 'NONE',  ( -16.98495255085919098, 65.99443563401679569, -56.88849027830389105 ) ) ;
#91117=CARTESIAN_POINT ( 'NONE',  ( -17.01825945287482966, 65.95000000001159890, -56.87310748452438958 ) ) ;
#91185=ADVANCED_FACE ( 'NONE', ( #17382 ), #72232, .F. ) ;
#91202=ORIENTED_EDGE ( 'NONE', *, *, #243846, .F. ) ;
#91262=EDGE_CURVE ( 'NONE', #94765, #13299, #16691, .T. ) ;
#91271=EDGE_CURVE ( 'NONE', #84975, #101180, #16120, .T. ) ;
#91320=FACE_OUTER_BOUND ( 'NONE', #245488, .T. ) ;
#91346=AXIS2_PLACEMENT_3D ( 'NONE', #158505, #218426, #235427 ) ;
#91354=CARTESIAN_POINT ( 'NONE',  ( -16.94225986326250677, 66.05000000001157900, -56.57638810891648973 ) ) ;
#91421=LINE ( 'NONE', #48425, #35331 ) ;
#91508=VERTEX_POINT ( 'NONE', #45925 ) ;
#91623=CARTESIAN_POINT ( 'NONE',  ( -16.81744102076748959, 66.05000000001153637, -48.67310748452439384 ) ) ;
#91638=( NAMED_UNIT ( * ) PLANE_ANGLE_UNIT ( ) SI_UNIT ( $, .RADIAN. ) );
#91703=VECTOR ( 'NONE', #125961, 1000.000000000000000 ) ;
#91742=CARTESIAN_POINT ( 'NONE',  ( -16.88460203013675098, 66.04524099677580296, -48.65721567498616906 ) ) ;
#91806=CARTESIAN_POINT ( 'NONE',  ( -17.29838795458828571, 65.62845014206074268, -47.41836620190301943 ) ) ;
#91928=B_SPLINE_CURVE_WITH_KNOTS ( 'NONE', 3,
 ( #183442, #106432, #85570, #244674 ),
 .UNSPECIFIED., .F., .F.,
 ( 4, 4 ),
 ( 0.000000000000000000, 7.713889350927385870E-05 ),
 .UNSPECIFIED. ) ;
#91941=CARTESIAN_POINT ( 'NONE',  ( -16.77977881697927032, 66.05339806647866396, -56.86172891140933672 ) ) ;
#91991=EDGE_CURVE ( 'NONE', #132612, #206343, #6598, .T. ) ;
#92128=EDGE_CURVE ( 'NONE', #53354, #212431, #120694, .T. ) ;
#92175=CARTESIAN_POINT ( 'NONE',  ( -15.73854595235691889, 66.64858632091015522, -52.54276391697543147 ) ) ;
#92240=EDGE_CURVE ( 'NONE', #176580, #90236, #123310, .T. ) ;
#92242=CARTESIAN_POINT ( 'NONE',  ( 15.06592377766032342, 66.58221053305935300, -54.16572294054753200 ) ) ;
#92267=EDGE_CURVE ( 'NONE', #86511, #206624, #50105, .T. ) ;
#92406=ORIENTED_EDGE ( 'NONE', *, *, #196241, .T. ) ;
#92409=ADVANCED_FACE ( 'NONE', ( #215596 ), #116520, .F. ) ;
#92436=VECTOR ( 'NONE', #157758, 1000.000000000000000 ) ;
#92491=EDGE_LOOP ( 'NONE', ( #188216, #60776, #253179, #48726 ) ) ;
#92604=CARTESIAN_POINT ( 'NONE',  ( -16.90137573187934095, 66.05000000001156479, -56.73469006042749641 ) ) ;
#92725=ORIENTED_EDGE ( 'NONE', *, *, #15246, .T. ) ;
#92783=CARTESIAN_POINT ( 'NONE',  ( -16.93440969289731157, 66.00481482419762358, -56.93187329951360454 ) ) ;
#93078=FACE_OUTER_BOUND ( 'NONE', #135353, .T. ) ;
#93131=B_SPLINE_CURVE_WITH_KNOTS ( 'NONE', 3,
 ( #110674, #151093, #230634, #191526 ),
 .UNSPECIFIED., .F., .F.,
 ( 4, 4 ),
 ( 0.000000000000000000, 7.713889350929220882E-05 ),
 .UNSPECIFIED. ) ;
#93450=CARTESIAN_POINT ( 'NONE',  ( -14.45422546970483957, 66.54939790392302257, -51.07921152142773025 ) ) ;
#93520=DIRECTION ( 'NONE',  ( 1.000000000000000000, 0.000000000000000000, 0.000000000000000000 ) ) ;
#93597=CARTESIAN_POINT ( 'NONE',  ( -23.25000000000000355, 70.35000000001159037, -56.87310748452436115 ) ) ;
#93688=CIRCLE ( 'NONE', #197730, 14.30833333333333890 ) ;
#94077=ORIENTED_EDGE ( 'NONE', *, *, #12279, .F. ) ;
#94189=( NAMED_UNIT ( * ) PLANE_ANGLE_UNIT ( ) SI_UNIT ( $, .RADIAN. ) );
#94252=CARTESIAN_POINT ( 'NONE',  ( -23.25000000000000355, 64.25000000001161027, -60.27310748452440947 ) ) ;
#94413=ORIENTED_EDGE ( 'NONE', *, *, #92267, .T. ) ;
#94609=DIRECTION ( 'NONE',  ( -1.000000000000000000, 4.625929269271478222E-14, 0.000000000000000000 ) ) ;
#94765=VERTEX_POINT ( 'NONE', #147822 ) ;
#94802=CARTESIAN_POINT ( 'NONE',  ( -14.00000000000000178, 66.15000000001155911, -52.77310748452439526 ) ) ;
#94815=CARTESIAN_POINT ( 'NONE',  ( -16.77683809663752257, 66.05416425680742520, -56.85915846542017960 ) ) ;
#94841=EDGE_LOOP ( 'NONE', ( #162156, #63985, #121656, #91202 ) ) ;
#94916=CARTESIAN_POINT ( 'NONE',  ( -17.04761207306817283, 65.97354912661374726, -48.67310748452440805 ) ) ;
#94949=ORIENTED_EDGE ( 'NONE', *, *, #191369, .T. ) ;
#95029=DIRECTION ( 'NONE',  ( 1.000000000000000000, -1.541976423090492636E-14, 0.000000000000000000 ) ) ;
#95162=PLANE ( 'NONE',  #167304 ) ;
#95273=ORIENTED_EDGE ( 'NONE', *, *, #34415, .T. ) ;
#95635=EDGE_CURVE ( 'NONE', #53354, #111912, #105464, .T. ) ;
#95674=PLANE ( 'NONE',  #123099 ) ;
#95716=DIRECTION ( 'NONE',  ( 1.186688945009010077E-16, 1.000000000000000000, 6.982962677686266711E-15 ) ) ;
#95851=VECTOR ( 'NONE', #73909, 1000.000000000000000 ) ;
#96101=CARTESIAN_POINT ( 'NONE',  ( -16.93589915522259304, 65.99137474131565284, -48.58254738256407990 ) ) ;
#96121=CARTESIAN_POINT ( 'NONE',  ( -18.40000000000000213, 70.35000000001159037, -56.87310748452436115 ) ) ;
#96255=CARTESIAN_POINT ( 'NONE',  ( 16.27683809663749770, 66.65000000001161595, -60.27310748452438816 ) ) ;
#96431=CARTESIAN_POINT ( 'NONE',  ( -17.11825945287481332, 65.95000000001152785, -48.67310748452439384 ) ) ;
#96616=VERTEX_POINT ( 'NONE', #88602 ) ;
#96824=ORIENTED_EDGE ( 'NONE', *, *, #79987, .F. ) ;
#96844=CIRCLE ( 'NONE', #117724, 0.09999999999999939493 ) ;
#97191=CARTESIAN_POINT ( 'NONE',  ( -14.11697426661281263, 66.54258905524415013, -54.52302351073435460 ) ) ;
#97249=ADVANCED_FACE ( 'NONE', ( #65559 ), #53236, .T. ) ;
#97365=CARTESIAN_POINT ( 'NONE',  ( -16.93344882324368683, 66.00341123272364996, -48.61008178971947302 ) ) ;
#97440=DIRECTION ( 'NONE',  ( -1.000000000000000000, -0.000000000000000000, -0.000000000000000000 ) ) ;
#97617=CARTESIAN_POINT ( 'NONE',  ( 20.05000000000002913, 68.75000000001158185, -60.27310748452437394 ) ) ;
#97652=EDGE_CURVE ( 'NONE', #90236, #239112, #160536, .T. ) ;
#97930=ORIENTED_EDGE ( 'NONE', *, *, #134142, .T. ) ;
#97939=CARTESIAN_POINT ( 'NONE',  ( -16.97683809663752186, 66.05000000001157900, -56.12074346632790878 ) ) ;
#97998=VECTOR ( 'NONE', #156972, 1000.000000000000000 ) ;
#98135=CARTESIAN_POINT ( 'NONE',  ( 14.45963434102924516, 66.54845833862603399, -51.06923198569381128 ) ) ;
#98366=FACE_OUTER_BOUND ( 'NONE', #239930, .T. ) ;
#98474=CARTESIAN_POINT ( 'NONE',  ( -13.54795643572458097, 66.54933111084403663, -54.46756099431704001 ) ) ;
#98576=VERTEX_POINT ( 'NONE', #206712 ) ;
#98824=DIRECTION ( 'NONE',  ( -1.000000000000000000, 0.000000000000000000, 0.000000000000000000 ) ) ;
#98912=LINE ( 'NONE', #175948, #146725 ) ;
#98950=CARTESIAN_POINT ( 'NONE',  ( -16.77683809663752257, 66.05416425680736836, -48.68705650362859672 ) ) ;
#99076=VERTEX_POINT ( 'NONE', #254187 ) ;
#99164=DIRECTION ( 'NONE',  ( -1.000000000000000000, -1.652117596168391700E-15, -1.153667551319263085E-29 ) ) ;
#99179=VERTEX_POINT ( 'NONE', #98950 ) ;
#99266=ORIENTED_EDGE ( 'NONE', *, *, #15246, .F. ) ;
#99287=CARTESIAN_POINT ( 'NONE',  ( -16.88815647973234135, 66.04916738069584881, -56.87589042119839888 ) ) ;
#99370=CARTESIAN_POINT ( 'NONE',  ( -16.80891096016324227, 66.05000000001157900, -56.89077029179306777 ) ) ;
#99410=VERTEX_POINT ( 'NONE', #94815 ) ;
#99431=CARTESIAN_POINT ( 'NONE',  ( -12.25000000000000178, 66.15000000001155911, -52.77310748452439526 ) ) ;
#99527=LINE ( 'NONE', #39625, #114835 ) ;
#99686=LINE ( 'NONE', #219653, #170398 ) ;
#99722=ORIENTED_EDGE ( 'NONE', *, *, #61977, .T. ) ;
#99875=ORIENTED_EDGE ( 'NONE', *, *, #182360, .T. ) ;
#99924=CARTESIAN_POINT ( 'NONE',  ( 15.74999999999999645, 66.65000000001155911, -52.77310748452439526 ) ) ;
#100031=SHAPE_REPRESENTATION ( 'Snap Open Cable Crossbars 15', ( #2425 ), #77591 ) ;
#100319=FACE_OUTER_BOUND ( 'NONE', #138203, .T. ) ;
#100629=CARTESIAN_POINT ( 'NONE',  ( -16.87683809663752399, 66.15000000001157332, -56.12074346632808641 ) ) ;
#100744=ORIENTED_EDGE ( 'NONE', *, *, #45161, .T. ) ;
#100756=VERTEX_POINT ( 'NONE', #56694 ) ;
#100866=ORIENTED_EDGE ( 'NONE', *, *, #86729, .F. ) ;
#101043=CARTESIAN_POINT ( 'NONE',  ( 23.24999999999999645, 67.17743825834520521, -60.27310748452438816 ) ) ;
#101057=DIRECTION ( 'NONE',  ( 0.000000000000000000, -1.000000000000000000, -6.789366196018718420E-15 ) ) ;
#101180=VERTEX_POINT ( 'NONE', #5410 ) ;
#101207=CARTESIAN_POINT ( 'NONE',  ( -16.94132844910800983, 66.00756324483117510, -48.62690572854207716 ) ) ;
#101287=VERTEX_POINT ( 'NONE', #1577 ) ;
#101354=LINE ( 'NONE', #79257, #38162 ) ;
#101545=LINE ( 'NONE', #140704, #92436 ) ;
#101773=ORIENTED_EDGE ( 'NONE', *, *, #77842, .F. ) ;
#101851=CARTESIAN_POINT ( 'NONE',  ( -16.87851181299898684, 66.04995707600383525, -56.87325099989131871 ) ) ;
#101923=CARTESIAN_POINT ( 'NONE',  ( -16.89268316805466341, 66.04827818676939444, -56.87885996306994230 ) ) ;
#101932=CARTESIAN_POINT ( 'NONE',  ( -16.83558968593870020, 66.05000000001157900, -56.86080229690766430 ) ) ;
#102238=EDGE_LOOP ( 'NONE', ( #213712, #11033, #132372, #204164 ) ) ;
#102435=ORIENTED_EDGE ( 'NONE', *, *, #167520, .T. ) ;
#102732=CARTESIAN_POINT ( 'NONE',  ( -18.44085059012131822, 64.48598750652780609, -60.26341280364594155 ) ) ;
#102781=EDGE_CURVE ( 'NONE', #37588, #84975, #116155, .T. ) ;
#102998=CYLINDRICAL_SURFACE ( 'NONE', #167004, 1.749999999999998002 ) ;
#103024=CARTESIAN_POINT ( 'NONE',  ( 18.54999999999999716, 67.25000000001156764, -60.27310748452438816 ) ) ;
#103127=ADVANCED_FACE ( 'NONE', ( #53292 ), #38872, .T. ) ;
#103133=DIRECTION ( 'NONE',  ( -1.000000000000000000, -7.125593699324843413E-30, 1.020425574104004196E-15 ) ) ;
#103143=CARTESIAN_POINT ( 'NONE',  ( -16.87331047859651179, 66.05000000001157900, -56.87310748452438958 ) ) ;
#103211=CARTESIAN_POINT ( 'NONE',  ( -16.80468759584937288, 66.05784632487743124, -56.83308861832274772 ) ) ;
#103224=CARTESIAN_POINT ( 'NONE',  ( -16.89155683852344936, 66.05000000001156479, -56.24573563498483963 ) ) ;
#103315=EDGE_CURVE ( 'NONE', #5771, #146300, #242181, .T. ) ;
#103366=CARTESIAN_POINT ( 'NONE',  ( -17.78043020864321022, 65.14640788800579685, -46.36005831880417816 ) ) ;
#103896=ORIENTED_EDGE ( 'NONE', *, *, #92128, .F. ) ;
#104109=CARTESIAN_POINT ( 'NONE',  ( -16.77180007708460963, 66.05000000001153637, -48.65872160347922204 ) ) ;
#104571=EDGE_LOOP ( 'NONE', ( #67665, #216913, #251070, #24290 ) ) ;
#104652=EDGE_CURVE ( 'NONE', #143115, #101180, #99527, .T. ) ;
#104783=CARTESIAN_POINT ( 'NONE',  ( -16.27683809663751191, 66.65000000001161595, -60.27310748452442368 ) ) ;
#104918=DIRECTION ( 'NONE',  ( -1.000000000000000000, 0.000000000000000000, -0.000000000000000000 ) ) ;
#105087=VECTOR ( 'NONE', #74304, 1000.000000000000000 ) ;
#105113=VERTEX_POINT ( 'NONE', #97939 ) ;
#105287=CARTESIAN_POINT ( 'NONE',  ( -12.48127053791145613, 66.62341902196760657, -51.89616123751247301 ) ) ;
#105301=ORIENTED_EDGE ( 'NONE', *, *, #110442, .T. ) ;
#105464=LINE ( 'NONE', #84607, #166118 ) ;
#105495=FACE_OUTER_BOUND ( 'NONE', #205793, .T. ) ;
#105950=CARTESIAN_POINT ( 'NONE',  ( -16.89797118371577866, 66.02361927736723146, -48.58581411696576424 ) ) ;
#106006=LINE ( 'NONE', #30370, #37624 ) ;
#106075=DIRECTION ( 'NONE',  ( 0.7071067811865487940, -0.7071067811865462405, -4.216150419019403701E-15 ) ) ;
#106389=ORIENTED_EDGE ( 'NONE', *, *, #49810, .T. ) ;
#106432=CARTESIAN_POINT ( 'NONE',  ( -18.40000000000000213, 64.52132590001160395, -45.29780070086501098 ) ) ;
#106586=CARTESIAN_POINT ( 'NONE',  ( -12.60829076262179882, 66.61047060254480812, -51.70599957163072702 ) ) ;
#107036=CARTESIAN_POINT ( 'NONE',  ( -16.97092634996638338, 65.99911103366348186, -56.89296471822659385 ) ) ;
#107257=EDGE_LOOP ( 'NONE', ( #150747, #225446, #169987 ) ) ;
#107380=FACE_OUTER_BOUND ( 'NONE', #80159, .T. ) ;
#107613=EDGE_LOOP ( 'NONE', ( #35958, #192036 ) ) ;
#107676=ADVANCED_FACE ( 'NONE', ( #133929 ), #15296, .F. ) ;
#107756=CARTESIAN_POINT ( 'NONE',  ( 18.39999999999999503, 64.52683809664902981, -48.67310748452440805 ) ) ;
#107805=EDGE_CURVE ( 'NONE', #68580, #145089, #191377, .T. ) ;
#108048=EDGE_LOOP ( 'NONE', ( #32732, #229274, #200258, #1308 ) ) ;
#108095=ORIENTED_EDGE ( 'NONE', *, *, #198967, .F. ) ;
#108170=ORIENTED_EDGE ( 'NONE', *, *, #52518, .T. ) ;
#108288=ORIENTED_EDGE ( 'NONE', *, *, #42890, .F. ) ;
#108839=CARTESIAN_POINT ( 'NONE',  ( -17.11825945287481332, 66.05000000001153637, -48.77310748452439526 ) ) ;
#108894=ORIENTED_EDGE ( 'NONE', *, *, #92240, .T. ) ;
#108991=ORIENTED_EDGE ( 'NONE', *, *, #18185, .T. ) ;
#109097=CARTESIAN_POINT ( 'NONE',  ( -16.94226253665225457, 66.05000000001155058, -48.96984208014017526 ) ) ;
#109349=CARTESIAN_POINT ( 'NONE',  ( 18.39999999999999503, 64.52683809664901560, -45.27310748452439526 ) ) ;
#109689=CARTESIAN_POINT ( 'NONE',  ( 15.48841904831874849, 67.43841904833030299, -48.67310748452437963 ) ) ;
#109754=AXIS2_PLACEMENT_3D ( 'NONE', #195599, #133048, #156486 ) ;
#110110=CYLINDRICAL_SURFACE ( 'NONE', #198673, 0.5000000000000004441 ) ;
#110136=MANIFOLD_SOLID_BREP ( 'Stock-MAS-200-1', #36934 ) ;
#110185=CARTESIAN_POINT ( 'NONE',  ( 21.72449340488909897, 65.71604372252039639, -48.67310748452440095 ) ) ;
#110201=ADVANCED_FACE ( 'NONE', ( #100319 ), #179902, .F. ) ;
#110214=CARTESIAN_POINT ( 'NONE',  ( -16.79814274880124358, 66.05072745733427553, -56.87067444747639655 ) ) ;
#110442=EDGE_CURVE ( 'NONE', #154587, #112394, #99686, .T. ) ;
#110474=ORIENTED_EDGE ( 'NONE', *, *, #242859, .F. ) ;
#110527=CARTESIAN_POINT ( 'NONE',  ( 14.22821877134046176, 66.54397173950364675, -54.51190944945866335 ) ) ;
#110674=CARTESIAN_POINT ( 'NONE',  ( -18.39999999999999858, 64.52683809664912928, -60.19716141771643692 ) ) ;
#110832=EDGE_CURVE ( 'NONE', #176630, #245188, #186530, .T. ) ;
#110871=EDGE_CURVE ( 'NONE', #243577, #214271, #113391, .T. ) ;
#111180=FACE_OUTER_BOUND ( 'NONE', #145351, .T. ) ;
#111521=ORIENTED_EDGE ( 'NONE', *, *, #30392, .T. ) ;
#111643=ORIENTED_EDGE ( 'NONE', *, *, #165632, .F. ) ;
#111830=CARTESIAN_POINT ( 'NONE',  ( 14.77516762759921853, 66.56332574816869396, -54.34624555352518627 ) ) ;
#111912=VERTEX_POINT ( 'NONE', #8243 ) ;
#111922=CARTESIAN_POINT ( 'NONE',  ( -20.65000000000000568, 70.35000000001160458, -60.27310748452436684 ) ) ;
#112394=VERTEX_POINT ( 'NONE', #246533 ) ;
#112665=DIRECTION ( 'NONE',  ( 1.000000000000000000, -1.186688945009010077E-16, -8.286604613020808509E-31 ) ) ;
#112775=LINE ( 'NONE', #252266, #55247 ) ;
#112791=AXIS2_PLACEMENT_3D ( 'NONE', #162884, #123738, #6335 ) ;
#112841=ADVANCED_FACE ( 'NONE', ( #156147 ), #33654, .F. ) ;
#113030=CARTESIAN_POINT ( 'NONE',  ( -15.66061380678752890, 66.63927620602552793, -52.20918028991767557 ) ) ;
#113104=CARTESIAN_POINT ( 'NONE',  ( 13.88302573338719093, 66.54258905524415013, -54.52302351073438302 ) ) ;
#113187=PLANE ( 'NONE',  #168202 ) ;
#113247=B_SPLINE_CURVE_WITH_KNOTS ( 'NONE', 3,
 ( #236767, #58116, #140222, #21600, #81521, #217197, #161108, #92783, #227163, #52365, #73270, #228474, #232332, #152806, #251859, #151513, #246722, #87643, #9397 ),
 .UNSPECIFIED., .F., .F.,
 ( 4, 3, 3, 3, 3, 3, 4 ),
 ( 0.0001624081864585766950, 0.0001685232196531723725, 0.0001764526673566880696, 0.0001916878551483189471, 0.0002009890782182605323, 0.0002238845907555128808, 0.0002283406619926333443 ),
 .UNSPECIFIED. ) ;
#113270=PLANE ( 'NONE',  #213700 ) ;
#113391=( BOUNDED_CURVE ( )  B_SPLINE_CURVE ( 3, ( #13046, #155133, #135512, #234631 ),
 .UNSPECIFIED., .F., .F. ) 
 B_SPLINE_CURVE_WITH_KNOTS ( ( 4, 4 ),
 ( 0.3000847527772391166, 0.5517402753107891744 ),
 .UNSPECIFIED. ) 
 CURVE ( )  GEOMETRIC_REPRESENTATION_ITEM ( )  RATIONAL_B_SPLINE_CURVE ( ( 1.000000000000000000, 0.9947294176030464508, 0.9947294176030464508, 1.000000000000000000 ) ) 
 REPRESENTATION_ITEM ( '' )  );
#113556=DIRECTION ( 'NONE',  ( 0.7071067811865463515, -0.7071067811865487940, -5.696443396193425170E-15 ) ) ;
#113757=( NAMED_UNIT ( * ) SI_UNIT ( $, .STERADIAN. ) SOLID_ANGLE_UNIT ( ) );
#113800=VECTOR ( 'NONE', #44861, 1000.000000000000000 ) ;
#113929=CARTESIAN_POINT ( 'NONE',  ( -17.27223548803035058, 65.65460260866045417, -47.38950130531501514 ) ) ;
#113933=DIRECTION ( 'NONE',  ( -1.186688945009010077E-16, -1.000000000000000000, -6.982962677686266711E-15 ) ) ;
#113982=B_SPLINE_CURVE_WITH_KNOTS ( 'NONE', 3,
 ( #236735, #217167, #17688, #81494, #201464, #39864, #38556, #197615, #240604, #239325, #61974, #141496, #97191, #60663, #200200, #98474, #221024, #78930, #21570, #140194, #178083, #257535, #222287, #42403, #158524, #238026 ),
 .UNSPECIFIED., .F., .F.,
 ( 4, 2, 2, 2, 2, 2, 2, 2, 2, 2, 2, 2, 4 ),
 ( 0.005476422646581357787, 0.006160811967703573935, 0.006845201288825792686, 0.007187395949386896424, 0.007529590609947999294, 0.007871785270509103899, 0.008213979931070206769, 0.008556174591631311374, 0.008898369252192415979, 0.009240563912753518849, 0.009582758573314621720, 0.01026714789443683266, 0.01095153721555904187 ),
 .UNSPECIFIED. ) ;
#114066=( BOUNDED_CURVE ( )  B_SPLINE_CURVE ( 3, ( #30813, #189858, #90740, #230258 ),
 .UNSPECIFIED., .F., .F. ) 
 B_SPLINE_CURVE_WITH_KNOTS ( ( 4, 4 ),
 ( 4.712388980384690562, 5.672655318024641069 ),
 .UNSPECIFIED. ) 
 CURVE ( )  GEOMETRIC_REPRESENTATION_ITEM ( )  RATIONAL_B_SPLINE_CURVE ( ( 1.000000000000000000, 0.9246222802177432865, 0.9246222802177432865, 1.000000000000000000 ) ) 
 REPRESENTATION_ITEM ( '' )  );
#114126=CARTESIAN_POINT ( 'NONE',  ( -16.87036670365549895, 66.01058118070993430, -57.00266760182645243 ) ) ;
#114835=VECTOR ( 'NONE', #38314, 1000.000000000000000 ) ;
#114934=VECTOR ( 'NONE', #164080, 1000.000000000000000 ) ;
#115048=EDGE_CURVE ( 'NONE', #96616, #37588, #240945, .T. ) ;
#115125=ORIENTED_EDGE ( 'NONE', *, *, #196603, .F. ) ;
#115291=LINE ( 'NONE', #57865, #198659 ) ;
#115523=ADVANCED_FACE ( 'NONE', ( #86335 ), #147625, .F. ) ;
#115610=AXIS2_PLACEMENT_3D ( 'NONE', #32518, #10363, #70354 ) ;
#116073=FILL_AREA_STYLE ('',( #36563 ) ) ;
#116155=LINE ( 'NONE', #33, #18795 ) ;
#116208=ORIENTED_EDGE ( 'NONE', *, *, #188434, .F. ) ;
#116318=ORIENTED_EDGE ( 'NONE', *, *, #256341, .T. ) ;
#116351=( NAMED_UNIT ( * ) SI_UNIT ( $, .STERADIAN. ) SOLID_ANGLE_UNIT ( ) );
#116466=CARTESIAN_POINT ( 'NONE',  ( 13.43663047529819998, 66.55335465531629779, -51.11230102842420564 ) ) ;
#116520=PLANE ( 'NONE',  #85859 ) ;
#116736=CARTESIAN_POINT ( 'NONE',  ( -33.72168855820452649, 64.52683809664912928, -60.27310748452440947 ) ) ;
#116745=LINE ( 'NONE', #235397, #189323 ) ;
#116779=PLANE ( 'NONE',  #249568 ) ;
#116818=DIRECTION ( 'NONE',  ( 1.186688945009009831E-16, 1.000000000000000000, 6.982962677686266711E-15 ) ) ;
#116868=CARTESIAN_POINT ( 'NONE',  ( -17.11825945287481687, 66.05000000001153637, -48.67310748452439384 ) ) ;
#116971=CARTESIAN_POINT ( 'NONE',  ( -16.93262454970419384, 65.99797953208116041, -48.59603125828708414 ) ) ;
#117096=ORIENTED_EDGE ( 'NONE', *, *, #1863, .F. ) ;
#117391=VECTOR ( 'NONE', #180155, 1000.000000000000000 ) ;
#117492=EDGE_CURVE ( 'NONE', #243170, #162196, #225278, .T. ) ;
#117643=ORIENTED_EDGE ( 'NONE', *, *, #18492, .F. ) ;
#117724=AXIS2_PLACEMENT_3D ( 'NONE', #37863, #215191, #36596 ) ;
#117941=DIRECTION ( 'NONE',  ( 0.000000000000000000, 0.000000000000000000, -1.000000000000000000 ) ) ;
#118035=LINE ( 'NONE', #109349, #225747 ) ;
#118356=CARTESIAN_POINT ( 'NONE',  ( -17.11825945287481332, 65.95000000001152785, -48.67310748452439384 ) ) ;
#118559=CARTESIAN_POINT ( 'NONE',  ( -20.65000000000000568, 68.75000000001159606, -56.87310748452436826 ) ) ;
#118576=CARTESIAN_POINT ( 'NONE',  ( -16.80469485234342031, 66.05784833687046387, -48.71314064059320970 ) ) ;
#118584=CARTESIAN_POINT ( 'NONE',  ( -16.89155683852731116, 66.05000000001420801, -49.30047933406498117 ) ) ;
#118766=CARTESIAN_POINT ( 'NONE',  ( 12.25000000000000000, 66.15000000001155911, -52.77310748452440237 ) ) ;
#118985=ADVANCED_FACE ( 'NONE', ( #55011 ), #18484, .T. ) ;
#119124=ADVANCED_FACE ( 'NONE', ( #62749 ), #202259, .F. ) ;
#119184=CIRCLE ( 'NONE', #123460, 0.1000000000000028644 ) ;
#119754=EDGE_CURVE ( 'NONE', #145079, #98576, #37615, .T. ) ;
#120024=TOROIDAL_SURFACE ( 'NONE', #187206, 14.20833333333334103, 0.1000000000000000056 ) ;
#120199=CARTESIAN_POINT ( 'NONE',  ( -16.87487986503753845, 66.04999244492597654, -56.87313274483766179 ) ) ;
#120206=LINE ( 'NONE', #23669, #117391 ) ;
#120349=CARTESIAN_POINT ( 'NONE',  ( 13.88638282980484107, 66.54257354752263609, -51.02306561612434876 ) ) ;
#120545=CARTESIAN_POINT ( 'NONE',  ( -21.65000000000000213, 68.75000000001161027, -60.27310748452437394 ) ) ;
#120694=LINE ( 'NONE', #101043, #189943 ) ;
#120974=VERTEX_POINT ( 'NONE', #228951 ) ;
#121026=DIRECTION ( 'NONE',  ( 0.000000000000000000, 1.000000000000000000, 6.982962677686266711E-15 ) ) ;
#121122=ORIENTED_EDGE ( 'NONE', *, *, #211038, .T. ) ;
#121564=CARTESIAN_POINT ( 'NONE',  ( -16.85697194749126382, 66.09145628588788668, -56.58810321691077405 ) ) ;
#121656=ORIENTED_EDGE ( 'NONE', *, *, #130200, .F. ) ;
#121869=CIRCLE ( 'NONE', #163553, 1.749999999999999778 ) ;
#122078=EDGE_CURVE ( 'NONE', #91508, #2351, #154885, .T. ) ;
#122129=ADVANCED_FACE ( 'NONE', ( #162023 ), #82429, .F. ) ;
#122321=VERTEX_POINT ( 'NONE', #169742 ) ;
#122719=CARTESIAN_POINT ( 'NONE',  ( -16.94107738177414291, 65.98576071487489969, -48.57310748452439952 ) ) ;
#122761=ADVANCED_FACE ( 'NONE', ( #37600 ), #113270, .F. ) ;
#122816=CARTESIAN_POINT ( 'NONE',  ( -16.80100426158789872, 66.05684947961542264, -56.84016173169033692 ) ) ;
#122984=ORIENTED_EDGE ( 'NONE', *, *, #219145, .F. ) ;
#122988=CARTESIAN_POINT ( 'NONE',  ( -16.87036670365548474, 66.01058118070986325, -48.54354736722234520 ) ) ;
#123099=AXIS2_PLACEMENT_3D ( 'NONE', #38288, #232651, #197342 ) ;
#123164=CARTESIAN_POINT ( 'NONE',  ( -16.94878442675512531, 66.00827089702058004, -56.91132706016227871 ) ) ;
#123300=VECTOR ( 'NONE', #229394, 1000.000000000000000 ) ;
#123310=CIRCLE ( 'NONE', #206516, 0.5000000000000004441 ) ;
#123460=AXIS2_PLACEMENT_3D ( 'NONE', #229106, #175567, #50437 ) ;
#123615=EDGE_CURVE ( 'NONE', #22343, #239112, #146013, .T. ) ;
#123669=DIRECTION ( 'NONE',  ( -0.000000000000000000, -6.982962677686266711E-15, 1.000000000000000000 ) ) ;
#123709=CARTESIAN_POINT ( 'NONE',  ( -16.83233564386398129, 66.06977820342696361, -48.79858682104877943 ) ) ;
#123738=DIRECTION ( 'NONE',  ( 1.000000000000000000, 0.000000000000000000, 0.000000000000000000 ) ) ;
#123823=CARTESIAN_POINT ( 'NONE',  ( 23.04999999999999716, 67.17743825834509153, -45.27310748452438816 ) ) ;
#123845=ORIENTED_EDGE ( 'NONE', *, *, #79987, .T. ) ;
#124112=CARTESIAN_POINT ( 'NONE',  ( -16.80621392010910498, 66.05779742250381048, -56.83351551910742927 ) ) ;
#124268=CARTESIAN_POINT ( 'NONE',  ( -16.97092634996639759, 65.99911103366341081, -48.65325025082221799 ) ) ;
#124271=CARTESIAN_POINT ( 'NONE',  ( -16.89318236219975589, 66.04846474213637464, -48.66797785241853802 ) ) ;
#124646=ORIENTED_EDGE ( 'NONE', *, *, #176347, .T. ) ;
#124770=CARTESIAN_POINT ( 'NONE',  ( 18.39999999999997371, 64.52683809664901560, -45.27310748452439526 ) ) ;
#124834=CARTESIAN_POINT ( 'NONE',  ( -16.86133551771148831, 66.05000000001155058, -48.72176404997775023 ) ) ;
#124900=CARTESIAN_POINT ( 'NONE',  ( -12.26136940704872202, 66.64859682586988754, -52.54357704768590054 ) ) ;
#124931=CARTESIAN_POINT ( 'NONE',  ( 18.39999999999999503, 70.35000000001153353, -48.67310748452436542 ) ) ;
#124940=AXIS2_PLACEMENT_3D ( 'NONE', #57780, #236432, #137321 ) ;
#124992=CARTESIAN_POINT ( 'NONE',  ( -16.89935556175728593, 66.05000000001153637, -49.16278384740906660 ) ) ;
#125116=FACE_OUTER_BOUND ( 'NONE', #184608, .T. ) ;
#125488=CARTESIAN_POINT ( 'NONE',  ( -16.87331047859649757, 66.05000000001153637, -48.67310748452439384 ) ) ;
#125601=CARTESIAN_POINT ( 'NONE',  ( 18.39999999999998082, 64.52683809664912928, -60.27310748452440947 ) ) ;
#125619=B_SPLINE_CURVE_WITH_KNOTS ( 'NONE', 3,
 ( #210419, #91742, #168765, #33095, #133434, #227389, #68330, #249543, #167450, #12224 ),
 .UNSPECIFIED., .F., .F.,
 ( 4, 3, 3, 4 ),
 ( 7.632826238683052976E-06, 4.756916949875583575E-05, 9.484459048150214273E-05, 0.0001435500935099850669 ),
 .UNSPECIFIED. ) ;
#125961=DIRECTION ( 'NONE',  ( 1.000000000000000000, 0.000000000000000000, 0.000000000000000000 ) ) ;
#126155=CARTESIAN_POINT ( 'NONE',  ( -12.30589683808040569, 66.64325398293328817, -52.31974776316020126 ) ) ;
#126213=CARTESIAN_POINT ( 'NONE',  ( -18.40000000000000213, 64.66825945288641719, -56.87310748452440379 ) ) ;
#126286=PLANE ( 'NONE',  #112791 ) ;
#126460=VECTOR ( 'NONE', #1350, 1000.000000000000000 ) ;
#126477=CIRCLE ( 'NONE', #197216, 0.9000000000000014655 ) ;
#126546=DIRECTION ( 'NONE',  ( 1.000000000000000000, 0.000000000000000000, 0.000000000000000000 ) ) ;
#126616=CARTESIAN_POINT ( 'NONE',  ( -17.11825945287482753, 65.95000000001159890, -56.87310748452439668 ) ) ;
#126826=CARTESIAN_POINT ( 'NONE',  ( -16.85718274719394572, 66.02385768538961486, -48.58645381670633867 ) ) ;
#126884=EDGE_LOOP ( 'NONE', ( #99266, #191677, #143759, #31937, #251743, #234693, #45528, #108170, #43619, #123845 ) ) ;
#126889=CARTESIAN_POINT ( 'NONE',  ( 23.04999999999999716, 67.17743825834520521, -60.27310748452438816 ) ) ;
#127097=ORIENTED_EDGE ( 'NONE', *, *, #52518, .F. ) ;
#127147=ORIENTED_EDGE ( 'NONE', *, *, #198049, .F. ) ;
#127376=VECTOR ( 'NONE', #220600, 1000.000000000000000 ) ;
#127516=STYLED_ITEM ( 'NONE', ( #195892 ), #178764 ) ;
#127551=CARTESIAN_POINT ( 'NONE',  ( -16.94052228080552069, 66.01372026691267081, -48.63273198185498103 ) ) ;
#127557=ORIENTED_EDGE ( 'NONE', *, *, #226356, .F. ) ;
#128061=CARTESIAN_POINT ( 'NONE',  ( -16.88593481969334320, 66.04943990992720160, -48.67123522757989917 ) ) ;
#128091=VERTEX_POINT ( 'NONE', #989 ) ;
#128161=CARTESIAN_POINT ( 'NONE',  ( 21.72449340488910607, 65.71604372252048165, -60.27310748452440237 ) ) ;
#128265=ORIENTED_EDGE ( 'NONE', *, *, #196241, .F. ) ;
#128539=VERTEX_POINT ( 'NONE', #243040 ) ;
#128593=CARTESIAN_POINT ( 'NONE',  ( -21.65000000000000213, 66.05000000001153637, -48.77310748452439526 ) ) ;
#128690=CARTESIAN_POINT ( 'NONE',  ( -16.92989507731676824, 66.05000000001152216, -48.90560855391422734 ) ) ;
#128837=CARTESIAN_POINT ( 'NONE',  ( 20.04999999999999716, 67.25000000001149658, -48.67310748452438673 ) ) ;
#128878=FACE_OUTER_BOUND ( 'NONE', #62590, .T. ) ;
#128898=EDGE_CURVE ( 'NONE', #253814, #145079, #207846, .T. ) ;
#129016=AXIS2_PLACEMENT_3D ( 'NONE', #3553, #166521, #162651 ) ;
#129294=CARTESIAN_POINT ( 'NONE',  ( -16.87331047859651179, 66.05000000001157900, -56.87310748452438958 ) ) ;
#129469=CARTESIAN_POINT ( 'NONE',  ( -16.77828822459933633, 66.05377062495506379, -48.68573573544333755 ) ) ;
#129657=ADVANCED_FACE ( 'NONE', ( #144116 ), #120024, .T. ) ;
#129761=DIRECTION ( 'NONE',  ( -1.000000000000000000, 1.646408749285562691E-14, 1.149681084847720908E-28 ) ) ;
#130059=EDGE_CURVE ( 'NONE', #19024, #241094, #239092, .T. ) ;
#130106=CARTESIAN_POINT ( 'NONE',  ( -16.86422026484316916, 66.02955263915092132, -56.94089425885139377 ) ) ;
#130198=VECTOR ( 'NONE', #233842, 1000.000000000000000 ) ;
#130200=EDGE_CURVE ( 'NONE', #139671, #101287, #253605, .T. ) ;
#130815=CARTESIAN_POINT ( 'NONE',  ( -18.40000000000000213, 64.52683809664910086, -56.97310748452440521 ) ) ;
#131095=VECTOR ( 'NONE', #64762, 1000.000000000000000 ) ;
#131247=ORIENTED_EDGE ( 'NONE', *, *, #54820, .T. ) ;
#131259=ADVANCED_FACE ( 'NONE', ( #111180 ), #29116, .T. ) ;
#131376=CARTESIAN_POINT ( 'NONE',  ( 12.25000000000000178, 66.65000000001154490, -53.00158811269929515 ) ) ;
#131390=CARTESIAN_POINT ( 'NONE',  ( -16.93521499325732549, 66.00521388020798952, -48.61599894343083861 ) ) ;
#131722=DIRECTION ( 'NONE',  ( 1.000000000000000000, 7.492892343619937423E-30, -1.073024830501117725E-15 ) ) ;
#132147=CARTESIAN_POINT ( 'NONE',  ( -23.25000000000000355, 65.95000000001152785, -48.77310748452439526 ) ) ;
#132284=CARTESIAN_POINT ( 'NONE',  ( -17.29158576265544056, 65.63525233399367664, -58.10586572931656946 ) ) ;
#132350=CARTESIAN_POINT ( 'NONE',  ( -16.78055652883087134, 66.05322308388622332, -56.86231564693196106 ) ) ;
#132357=( BOUNDED_SURFACE ( )  B_SPLINE_SURFACE ( 3, 2, ( 
 ( #191764, #27559, #126616 ),
 ( #225679, #249152, #70530 ),
 ( #151341, #247848, #107036 ),
 ( #148763, #186608, #10533 ) ),
 .UNSPECIFIED., .F., .F., .F. ) 
 B_SPLINE_SURFACE_WITH_KNOTS ( ( 4, 4 ),
 ( 3, 3 ),
 ( 4.712388980384689674, 5.765869716888459173 ),
 ( 0.000000000000000000, 1.000000000000000000 ),
 .UNSPECIFIED. ) 
 GEOMETRIC_REPRESENTATION_ITEM ( )  RATIONAL_B_SPLINE_SURFACE ( (
 ( 1.000000000000000000, 0.7071067811865719976, 1.000000000000000000),
 ( 1.000000000000000000, 0.7953136715913269317, 1.000000000000000000),
 ( 1.000000000000000000, 0.8646876308615392137, 1.000000000000000000),
 ( 1.000000000000000000, 0.8984936768950618768, 1.000000000000000000) ) ) 
 REPRESENTATION_ITEM ( '' )  SURFACE ( )  );
#132372=ORIENTED_EDGE ( 'NONE', *, *, #130059, .T. ) ;
#132402=EDGE_CURVE ( 'NONE', #65805, #89456, #144579, .T. ) ;
#132612=VERTEX_POINT ( 'NONE', #99431 ) ;
#132651=CARTESIAN_POINT ( 'NONE',  ( 18.54999999999999716, 67.25000000001149658, -48.67310748452438673 ) ) ;
#132694=CARTESIAN_POINT ( 'NONE',  ( -16.94389599337535657, 66.00880201025478300, -48.63075228632278169 ) ) ;
#132779=CARTESIAN_POINT ( 'NONE',  ( 23.24999999999999645, 64.25000000001161027, -60.27310748452440947 ) ) ;
#132838=CARTESIAN_POINT ( 'NONE',  ( 20.04999999999999716, 67.25000000001158185, -60.27310748452438816 ) ) ;
#133048=DIRECTION ( 'NONE',  ( -1.000000000000000000, 0.000000000000000000, -0.000000000000000000 ) ) ;
#133194=CIRCLE ( 'NONE', #20793, 1.500000000000001332 ) ;
#133311=LINE ( 'NONE', #212850, #248269 ) ;
#133434=CARTESIAN_POINT ( 'NONE',  ( -16.86733706339143524, 66.03400947037184210, -48.61999218252569932 ) ) ;
#133637=CARTESIAN_POINT ( 'NONE',  ( -16.77683809663752257, 66.05416425680742520, -56.85915846542017960 ) ) ;
#133929=FACE_OUTER_BOUND ( 'NONE', #85423, .T. ) ;
#133938=CARTESIAN_POINT ( 'NONE',  ( 14.56326696814972088, 66.55335100938272319, -54.43394418860123096 ) ) ;
#134142=EDGE_CURVE ( 'NONE', #190074, #2351, #22237, .T. ) ;
#134696=CIRCLE ( 'NONE', #9627, 0.09999999999999939493 ) ;
#134715=CARTESIAN_POINT ( 'NONE',  ( 12.33938619321247465, 66.63927620602551372, -52.20918028991769688 ) ) ;
#134891=CARTESIAN_POINT ( 'NONE',  ( -16.80438519320023616, 66.05022090354323439, -56.87236920360312098 ) ) ;
#135051=AXIS2_PLACEMENT_3D ( 'NONE', #238101, #179443, #59434 ) ;
#135097=ORIENTED_EDGE ( 'NONE', *, *, #141046, .F. ) ;
#135160=DIRECTION ( 'NONE',  ( 0.000000000000000000, 0.000000000000000000, 1.000000000000000000 ) ) ;
#135215=CARTESIAN_POINT ( 'NONE',  ( -16.90257928357874917, 66.04589317890619782, -56.88682205441069328 ) ) ;
#135353=EDGE_LOOP ( 'NONE', ( #35522, #26949, #62256, #87177, #128265 ) ) ;
#135512=CARTESIAN_POINT ( 'NONE',  ( -17.71734398241074260, 65.15764277154693218, -46.29796923151879895 ) ) ;
#135528=VECTOR ( 'NONE', #157162, 1000.000000000000000 ) ;
#135628=ORIENTED_EDGE ( 'NONE', *, *, #138512, .T. ) ;
#135995=CARTESIAN_POINT ( 'NONE',  ( 15.57250062127602597, 66.62931007840892050, -51.99664235786332256 ) ) ;
#136035=ORIENTED_EDGE ( 'NONE', *, *, #182360, .F. ) ;
#136130=DIRECTION ( 'NONE',  ( 0.5932847527679299127, 0.8049926720990051576, 4.984624513800587583E-15 ) ) ;
#136493=CARTESIAN_POINT ( 'NONE',  ( -16.92132318717937522, 66.03392997600563774, -56.90070085417232804 ) ) ;
#136777=LINE ( 'NONE', #199344, #211598 ) ;
#136792=AXIS2_PLACEMENT_3D ( 'NONE', #181201, #225418, #145889 ) ;
#137036=CARTESIAN_POINT ( 'NONE',  ( -21.64999999999999858, 66.65000000001161595, -60.27310748452439526 ) ) ;
#137321=DIRECTION ( 'NONE',  ( -1.000000000000000000, 0.000000000000000000, 0.000000000000000000 ) ) ;
#137460=CARTESIAN_POINT ( 'NONE',  ( -18.40000000000000213, 64.52683809664902981, -48.57310748452440663 ) ) ;
#137490=DIRECTION ( 'NONE',  ( -1.000000000000000000, 0.000000000000000000, -0.000000000000000000 ) ) ;
#137656=DIRECTION ( 'NONE',  ( -1.020425574104004196E-15, -6.982962677686266711E-15, 1.000000000000000000 ) ) ;
#138099=CARTESIAN_POINT ( 'NONE',  ( -16.77683809663752257, 66.05416425680736836, -48.68705650362859672 ) ) ;
#138203=EDGE_LOOP ( 'NONE', ( #131247, #72690, #236954, #69191 ) ) ;
#138395=DIRECTION ( 'NONE',  ( 1.000000000000000000, -1.186688945009009831E-16, -8.286604613020806758E-31 ) ) ;
#138399=VECTOR ( 'NONE', #131, 1000.000000000000000 ) ;
#138491=CARTESIAN_POINT ( 'NONE',  ( -16.80070461187911590, 66.05000000001234639, -56.87614365536322936 ) ) ;
#138512=EDGE_CURVE ( 'NONE', #148974, #176630, #160796, .T. ) ;
#138554=CARTESIAN_POINT ( 'NONE',  ( 15.74999999999999645, 66.65000000001155911, -52.77310748452439526 ) ) ;
#139182=PRODUCT_DEFINITION_CONTEXT ( 'detailed design', #245812, 'design' ) ;
#139333=DIRECTION ( 'NONE',  ( 1.000000000000000000, 0.000000000000000000, 0.000000000000000000 ) ) ;
#139467=CARTESIAN_POINT ( 'NONE',  ( -18.40000000000000213, 64.66825945288641719, -56.87310748452440379 ) ) ;
#139671=VERTEX_POINT ( 'NONE', #59100 ) ;
#139746=LINE ( 'NONE', #181484, #127376 ) ;
#139852=CARTESIAN_POINT ( 'NONE',  ( 15.74999999999999289, 66.65000000001155911, -52.65736431725049016 ) ) ;
#139987=EDGE_LOOP ( 'NONE', ( #54420, #243785, #224727, #59941 ) ) ;
#140033=AXIS2_PLACEMENT_3D ( 'NONE', #68128, #54953, #90231 ) ;
#140090=CARTESIAN_POINT ( 'NONE',  ( -33.72168855820452649, 52.34166666667822199, -52.77310748452448763 ) ) ;
#140194=CARTESIAN_POINT ( 'NONE',  ( -12.93407622233968191, 66.58221053305935300, -54.16572294054751779 ) ) ;
#140222=CARTESIAN_POINT ( 'NONE',  ( -16.94180778212363236, 66.00755694427942899, -56.91892391399115070 ) ) ;
#140286=CARTESIAN_POINT ( 'NONE',  ( -16.87683809663752399, 66.15000000001153069, -49.42547150272069700 ) ) ;
#140353=CARTESIAN_POINT ( 'NONE',  ( -16.92925196614875105, 66.02766820360145061, -56.90636263680760010 ) ) ;
#140450=VECTOR ( 'NONE', #66343, 1000.000000000000000 ) ;
#140570=EDGE_CURVE ( 'NONE', #230076, #163978, #113982, .T. ) ;
#140704=CARTESIAN_POINT ( 'NONE',  ( -21.65000000000000213, 66.05000000001157900, -56.87310748452438958 ) ) ;
#140968=ORIENTED_EDGE ( 'NONE', *, *, #157557, .F. ) ;
#141027=DIRECTION ( 'NONE',  ( -0.7071067811865456854, -0.7071067811865493491, -4.937700262164544098E-15 ) ) ;
#141046=EDGE_CURVE ( 'NONE', #112394, #14611, #35944, .T. ) ;
#141050=DIRECTION ( 'NONE',  ( 0.000000000000000000, -6.982962677686266711E-15, 1.000000000000000000 ) ) ;
#141079=LINE ( 'NONE', #41994, #207566 ) ;
#141100=CARTESIAN_POINT ( 'NONE',  ( -16.79270642812310399, 66.05375578307352669, -56.86204076308684563 ) ) ;
#141429=CARTESIAN_POINT ( 'NONE',  ( -16.89318236219976654, 66.04846474213643148, -56.87823711663025250 ) ) ;
#141496=CARTESIAN_POINT ( 'NONE',  ( -14.23072895065542198, 66.54401276639880791, -54.51157631762654887 ) ) ;
#141535=ORIENTED_EDGE ( 'NONE', *, *, #74058, .F. ) ;
#141746=ORIENTED_EDGE ( 'NONE', *, *, #141046, .T. ) ;
#141969=CARTESIAN_POINT ( 'NONE',  ( -16.85697194749128514, 66.09145628588790089, -48.95811175213842148 ) ) ;
#142044=PLANE ( 'NONE',  #136792 ) ;
#142198=ADVANCED_FACE ( 'NONE', ( #188077 ), #148965, .F. ) ;
#142283=CARTESIAN_POINT ( 'NONE',  ( -16.88219499860498374, 66.04979357458398681, -56.87379779441709360 ) ) ;
#142690=CARTESIAN_POINT ( 'NONE',  ( -17.11825945287481332, 66.05000000001153637, -48.77310748452439526 ) ) ;
#142899=CIRCLE ( 'NONE', #205453, 0.1000000000000028644 ) ;
#143069=DIRECTION ( 'NONE',  ( 0.7071067811865463515, 0.7071067811865487940, 4.937700262164540154E-15 ) ) ;
#143115=VERTEX_POINT ( 'NONE', #152209 ) ;
#143210=CARTESIAN_POINT ( 'NONE',  ( 20.27550659511088682, 66.78395627750272467, -56.87310748452438247 ) ) ;
#143458=ORIENTED_EDGE ( 'NONE', *, *, #246576, .F. ) ;
#143759=ORIENTED_EDGE ( 'NONE', *, *, #70424, .T. ) ;
#143946=LINE ( 'NONE', #223478, #113800 ) ;
#144116=FACE_OUTER_BOUND ( 'NONE', #139987, .T. ) ;
#144426=CARTESIAN_POINT ( 'NONE',  ( -17.73285935861365203, 65.14201819622128653, -59.28166929430445009 ) ) ;
#144448=VECTOR ( 'NONE', #257015, 1000.000000000000000 ) ;
#144528=CARTESIAN_POINT ( 'NONE',  ( -16.77308656112215246, 66.05000000001153637, -48.67330067622668821 ) ) ;
#144579=( BOUNDED_CURVE ( )  B_SPLINE_CURVE ( 3, ( #252102, #249558, #194731, #16096 ),
 .UNSPECIFIED., .F., .F. ) 
 B_SPLINE_CURVE_WITH_KNOTS ( ( 4, 4 ),
 ( -9.769962616701377556E-15, 1.570796326794891673 ),
 .UNSPECIFIED. ) 
 CURVE ( )  GEOMETRIC_REPRESENTATION_ITEM ( )  RATIONAL_B_SPLINE_CURVE ( ( 1.000000000000000000, 0.8047378541243637162, 0.8047378541243637162, 1.000000000000000000 ) ) 
 REPRESENTATION_ITEM ( '' )  );
#144612=CARTESIAN_POINT ( 'NONE',  ( -15.75000000000000355, 66.15000000001155911, -52.77310748452439526 ) ) ;
#144771=ORIENTED_EDGE ( 'NONE', *, *, #229422, .F. ) ;
#144881=ORIENTED_EDGE ( 'NONE', *, *, #15520, .T. ) ;
#145074=ORIENTED_EDGE ( 'NONE', *, *, #200150, .F. ) ;
#145079=VERTEX_POINT ( 'NONE', #122719 ) ;
#145089=VERTEX_POINT ( 'NONE', #146103 ) ;
#145172=EDGE_LOOP ( 'NONE', ( #197374, #208576, #1831, #111643, #5753 ) ) ;
#145305=( BOUNDED_SURFACE ( )  B_SPLINE_SURFACE ( 3, 2, ( 
 ( #237232, #58568, #59845 ),
 ( #39047, #118584, #165401 ),
 ( #45445, #124992, #244924 ),
 ( #141969, #84519, #204505 ),
 ( #65000, #83256, #2451 ),
 ( #123709, #201960, #67573 ),
 ( #164120, #6303, #246218 ),
 ( #222779, #3749, #44176 ),
 ( #241101, #24631, #226634 ),
 ( #23348, #144528, #104109 ) ),
 .UNSPECIFIED., .F., .F., .F. ) 
 B_SPLINE_SURFACE_WITH_KNOTS ( ( 4, 2, 2, 2, 4 ),
 ( 3, 3 ),
 ( 0.002161241639767248670, 0.002579950749615824400, 0.002789305304540112482, 0.002893982582002256523, 0.002998659859464400564 ),
 ( 0.000000000000000000, 1.000000000000000000 ),
 .UNSPECIFIED. ) 
 GEOMETRIC_REPRESENTATION_ITEM ( )  RATIONAL_B_SPLINE_SURFACE ( (
 ( 1.000000000000000000, 0.7071067811865475727, 1.000000000000000000),
 ( 1.000000000000000000, 0.7632447400665651749, 1.000000000000000000),
 ( 1.000000000000000000, 0.8158073005108548159, 1.000000000000000000),
 ( 1.000000000000000000, 0.8906973462396701180, 1.000000000000000000),
 ( 1.000000000000000000, 0.9149408947804169578, 1.000000000000000000),
 ( 1.000000000000000000, 0.9493368785273816890, 1.000000000000000000),
 ( 1.000000000000000000, 0.9605194247156174647, 1.000000000000000000),
 ( 1.000000000000000000, 0.9803630264781744152, 1.000000000000000000),
 ( 1.000000000000000000, 0.9900844824270682576, 1.000000000000000000),
 ( 1.000000000000000000, 0.9894588281429290699, 1.000000000000000000) ) ) 
 REPRESENTATION_ITEM ( '' )  SURFACE ( )  );
#145351=EDGE_LOOP ( 'NONE', ( #103896, #255103, #53553, #256673 ) ) ;
#145365=CIRCLE ( 'NONE', #70404, 0.09999999999999516220 ) ;
#145386=COLOUR_RGB ( '', 0.08235294, 0.09019608, 0.10196078) ;
#145465=DIRECTION ( 'NONE',  ( -1.646408749285562691E-14, -1.000000000000000000, -6.982962677686266711E-15 ) ) ;
#145597=CARTESIAN_POINT ( 'NONE',  ( 18.39999999999999503, 64.25000000001151079, -45.27310748452440237 ) ) ;
#145889=DIRECTION ( 'NONE',  ( 1.000000000000000000, -1.186688945009009831E-16, -8.286604613020806758E-31 ) ) ;
#146013=LINE ( 'NONE', #180030, #26658 ) ;
#146103=CARTESIAN_POINT ( 'NONE',  ( -20.65000000000000568, 68.75000000001159606, -56.87310748452436826 ) ) ;
#146300=VERTEX_POINT ( 'NONE', #168336 ) ;
#146435=CARTESIAN_POINT ( 'NONE',  ( -16.80117486205003630, 66.05034273169920311, -48.67425261159890937 ) ) ;
#146475=ORIENTED_EDGE ( 'NONE', *, *, #226356, .T. ) ;
#146725=VECTOR ( 'NONE', #139333, 1000.000000000000000 ) ;
#146788=ORIENTED_EDGE ( 'NONE', *, *, #88758, .T. ) ;
#146930=ORIENTED_EDGE ( 'NONE', *, *, #7601, .T. ) ;
#146934=CARTESIAN_POINT ( 'NONE',  ( -16.97683809663753252, 66.05000000001152216, -49.29463665241382131 ) ) ;
#147064=ORIENTED_EDGE ( 'NONE', *, *, #203096, .F. ) ;
#147625=PLANE ( 'NONE',  #205062 ) ;
#147822=CARTESIAN_POINT ( 'NONE',  ( 16.87683809663749557, 66.05000000001155058, -48.67310748452439384 ) ) ;
#147962=FACE_OUTER_BOUND ( 'NONE', #21782, .T. ) ;
#148309=CARTESIAN_POINT ( 'NONE',  ( -15.69373346032659100, 66.64320997496565724, -52.31828097591049698 ) ) ;
#148407=ADVANCED_FACE ( 'NONE', ( #93078 ), #8277, .T. ) ;
#148516=CARTESIAN_POINT ( 'NONE',  ( -18.38639463286148867, 64.51980042617562106, -60.27310748452440947 ) ) ;
#148610=CARTESIAN_POINT ( 'NONE',  ( -21.65000000000000213, 68.75000000001153921, -48.67310748452437252 ) ) ;
#148763=CARTESIAN_POINT ( 'NONE',  ( -16.87242674293850797, 66.05000000001159322, -56.87419773089673924 ) ) ;
#148928=DIRECTION ( 'NONE',  ( 0.000000000000000000, 1.000000000000000000, 6.982962677686266711E-15 ) ) ;
#148965=CYLINDRICAL_SURFACE ( 'NONE', #140033, 0.1000000000000038219 ) ;
#148974=VERTEX_POINT ( 'NONE', #63286 ) ;
#149144=CIRCLE ( 'NONE', #182458, 14.30833333333333890 ) ;
#149162=ORIENTED_EDGE ( 'NONE', *, *, #192345, .F. ) ;
#149308=DIRECTION ( 'NONE',  ( -0.5932847527679299127, -0.8049926720990051576, -6.257843056355997642E-15 ) ) ;
#149549=CARTESIAN_POINT ( 'NONE',  ( -16.97683809663752186, 66.05000000001155058, -49.42547150272071121 ) ) ;
#149781=DIRECTION ( 'NONE',  ( 0.2834754621636439431, 0.2834754621636471628, 0.9161240771326858434 ) ) ;
#149815=PLANE ( 'NONE',  #55710 ) ;
#149882=CARTESIAN_POINT ( 'NONE',  ( -20.65000000000000568, 70.35000000001159037, -56.87310748452436115 ) ) ;
#150018=ORIENTED_EDGE ( 'NONE', *, *, #92240, .F. ) ;
#150087=CARTESIAN_POINT ( 'NONE',  ( 20.05000000000002913, 68.75000000001149658, -48.67310748452437963 ) ) ;
#150169=CARTESIAN_POINT ( 'NONE',  ( 12.25000000000000000, 66.15000000001155911, -52.77310748452439526 ) ) ;
#150327=CARTESIAN_POINT ( 'NONE',  ( -16.77779411440718604, 66.05389855290391665, -48.68616490152893306 ) ) ;
#150466=LINE ( 'NONE', #155623, #130198 ) ;
#150557=VECTOR ( 'NONE', #54553, 1000.000000000000000 ) ;
#150607=EDGE_CURVE ( 'NONE', #111912, #128539, #65596, .T. ) ;
#150658=VECTOR ( 'NONE', #97440, 1000.000000000000000 ) ;
#150747=ORIENTED_EDGE ( 'NONE', *, *, #49493, .F. ) ;
#150843=ORIENTED_EDGE ( 'NONE', *, *, #60601, .F. ) ;
#150894=ORIENTED_EDGE ( 'NONE', *, *, #53194, .F. ) ;
#150952=CARTESIAN_POINT ( 'NONE',  ( 14.11444803880196552, 66.54256847116262463, -54.52319054662471842 ) ) ;
#151083=CARTESIAN_POINT ( 'NONE',  ( 18.39999999999999503, 70.35000000001159037, -56.87310748452436115 ) ) ;
#151093=CARTESIAN_POINT ( 'NONE',  ( -18.39999999999999858, 64.52683809664912928, -60.22327823605839825 ) ) ;
#151341=CARTESIAN_POINT ( 'NONE',  ( -16.92209698673576668, 66.05000000001159322, -56.81247191747281988 ) ) ;
#151361=ADVANCED_FACE ( 'NONE', ( #165480 ), #142044, .T. ) ;
#151513=CARTESIAN_POINT ( 'NONE',  ( -16.93906926870270624, 65.98785312906501588, -56.96965517729757522 ) ) ;
#151640=SURFACE_STYLE_FILL_AREA ( #212876 ) ;
#151803=CARTESIAN_POINT ( 'NONE',  ( -16.91256925476570672, 66.01426884188333588, -48.55546499551912376 ) ) ;
#152158=ORIENTED_EDGE ( 'NONE', *, *, #229824, .T. ) ;
#152209=CARTESIAN_POINT ( 'NONE',  ( 18.54999999999999716, 66.05000000001156479, -56.87310748452444642 ) ) ;
#152248=DIRECTION ( 'NONE',  ( 1.186688945009010077E-16, 1.000000000000000000, 6.982962677686266711E-15 ) ) ;
#152258=CARTESIAN_POINT ( 'NONE',  ( 12.93225390519044993, 66.58234804117054750, -54.16432009208397602 ) ) ;
#152273=CARTESIAN_POINT ( 'NONE',  ( -16.92563707711778065, 66.03100930561473092, -48.64234918500041971 ) ) ;
#152293=DIRECTION ( 'NONE',  ( -0.000000000000000000, -6.982962677686266711E-15, 1.000000000000000000 ) ) ;
#152342=CARTESIAN_POINT ( 'NONE',  ( -18.40000000000000213, 64.52683809664910086, -56.87310748452440379 ) ) ;
#152387=UNCERTAINTY_MEASURE_WITH_UNIT (LENGTH_MEASURE( 1.000000000000000082E-05 ), #172512, 'distance_accuracy_value', 'NONE');
#152620=ADVANCED_FACE ( 'NONE', ( #105495 ), #6425, .F. ) ;
#152806=CARTESIAN_POINT ( 'NONE',  ( -16.93339986808596720, 65.99489607144565184, -56.95711381271154039 ) ) ;
#152957=CARTESIAN_POINT ( 'NONE',  ( 18.39999999999998082, 64.52683809664912928, -60.27310748452440947 ) ) ;
#153495=CARTESIAN_POINT ( 'NONE',  ( -15.51798037960204546, 66.62334006147798959, -51.89491493630710295 ) ) ;
#153513=CARTESIAN_POINT ( 'NONE',  ( 0.000000000000000000, 0.000000000000000000, 0.000000000000000000 ) ) ;
#153702=VECTOR ( 'NONE', #11257, 1000.000000000000000 ) ;
#153936=CYLINDRICAL_SURFACE ( 'NONE', #236319, 1.749999999999998002 ) ;
#154173=AXIS2_PLACEMENT_3D ( 'NONE', #257056, #141027, #57607 ) ;
#154547=ORIENTED_EDGE ( 'NONE', *, *, #196238, .F. ) ;
#154587=VERTEX_POINT ( 'NONE', #258031 ) ;
#154708=DIRECTION ( 'NONE',  ( 1.186688945009010077E-16, 1.000000000000000000, 6.982962677686266711E-15 ) ) ;
#154838=CARTESIAN_POINT ( 'NONE',  ( -16.94107738177414291, 65.98576071487489969, -48.57310748452439952 ) ) ;
#154885=B_SPLINE_CURVE_WITH_KNOTS ( 'NONE', 3,
 ( #138554, #139852, #197274, #233840, #173912, #135995, #215548, #18639, #77314, #39524, #36956, #98135, #177744, #120349, #156898, #74806, #116466, #55159, #196007, #17364, #257195, #158197, #57749, #175196, #78601, #134715, #214278, #194736, #237690, #254647 ),
 .UNSPECIFIED., .F., .F.,
 ( 4, 2, 2, 2, 2, 2, 2, 2, 2, 2, 2, 2, 2, 2, 4 ),
 ( 0.000000000000000000, 0.0003422764154113329101, 0.0006845528308226658202, 0.001026829246233998839, 0.001369105661645331640, 0.002053658492468003749, 0.002738211323290675424, 0.003080487738702009093, 0.003422764154113342328, 0.003765040569524676431, 0.004107316984936010100, 0.004449593400347342902, 0.004791869815758676571, 0.005134146231170010240, 0.005476422646581343909 ),
 .UNSPECIFIED. ) ;
#155010=B_SPLINE_CURVE_WITH_KNOTS ( 'NONE', 3,
 ( #64840, #223904, #124834, #247330, #66132, #128690, #109097, #70012, #146934, #149549 ),
 .UNSPECIFIED., .F., .F.,
 ( 4, 2, 2, 2, 4 ),
 ( 5.259846352425386116E-16, 9.930191194500792909E-05, 0.0001986038238894898575, 0.0003972076477784336566, 0.0007944152955563403909 ),
 .UNSPECIFIED. ) ;
#155105=DIRECTION ( 'NONE',  ( -0.7071067811865463515, -0.7071067811865487940, -4.937700262164540154E-15 ) ) ;
#155133=CARTESIAN_POINT ( 'NONE',  ( -17.22361732159831860, 65.65484434140907410, -47.39389201039153221 ) ) ;
#155327=AXIS2_PLACEMENT_3D ( 'NONE', #240766, #24297, #2126 ) ;
#155623=CARTESIAN_POINT ( 'NONE',  ( -18.40000000000000213, 67.17743825834509153, -45.27310748452438816 ) ) ;
#155754=EDGE_LOOP ( 'NONE', ( #67813, #72441, #214711, #161684, #53856, #209814, #54718, #206340, #143458, #236098, #193477, #164151 ) ) ;
#156113=CARTESIAN_POINT ( 'NONE',  ( 13.12220780326572012, 66.56936653093875123, -54.29134168970031737 ) ) ;
#156127=CARTESIAN_POINT ( 'NONE',  ( -16.93353400591625757, 65.99538760383858005, -48.59042301431898636 ) ) ;
#156147=FACE_OUTER_BOUND ( 'NONE', #242044, .T. ) ;
#156179=ORIENTED_EDGE ( 'NONE', *, *, #117492, .T. ) ;
#156343=ADVANCED_FACE ( 'NONE', ( #218033 ), #36478, .F. ) ;
#156437=CARTESIAN_POINT ( 'NONE',  ( -16.81931177881021711, 66.06300394050762748, -48.74988960590717113 ) ) ;
#156486=DIRECTION ( 'NONE',  ( 0.000000000000000000, 6.982962677686266711E-15, -1.000000000000000000 ) ) ;
#156676=ORIENTED_EDGE ( 'NONE', *, *, #18492, .T. ) ;
#156714=VERTEX_POINT ( 'NONE', #256819 ) ;
#156757=FACE_OUTER_BOUND ( 'NONE', #8104, .T. ) ;
#156836=DIRECTION ( 'NONE',  ( -1.000000000000000000, 0.000000000000000000, 0.000000000000000000 ) ) ;
#156898=CARTESIAN_POINT ( 'NONE',  ( 13.77030915526558275, 66.54399267394222761, -51.03447399037763432 ) ) ;
#156971=FACE_OUTER_BOUND ( 'NONE', #126884, .T. ) ;
#156972=DIRECTION ( 'NONE',  ( 1.186688945009010077E-16, 1.000000000000000000, 6.982962677686266711E-15 ) ) ;
#157162=DIRECTION ( 'NONE',  ( -0.7071067811865456854, -0.7071067811865493491, -4.937700262164544098E-15 ) ) ;
#157188=DIRECTION ( 'NONE',  ( 0.000000000000000000, -1.000000000000000000, -6.982962677686266711E-15 ) ) ;
#157192=DIRECTION ( 'NONE',  ( 0.000000000000000000, -6.982962677686266711E-15, 1.000000000000000000 ) ) ;
#157405=CARTESIAN_POINT ( 'NONE',  ( -16.91247567987037925, 66.04091731634233042, -56.89438302598705377 ) ) ;
#157557=EDGE_CURVE ( 'NONE', #89456, #78170, #116745, .T. ) ;
#157753=DIRECTION ( 'NONE',  ( -1.020425574104004196E-15, 6.982962677686266711E-15, -1.000000000000000000 ) ) ;
#157758=DIRECTION ( 'NONE',  ( 0.000000000000000000, 6.982962677686266711E-15, -1.000000000000000000 ) ) ;
#158122=LINE ( 'NONE', #237619, #193563 ) ;
#158197=CARTESIAN_POINT ( 'NONE',  ( 12.68104795156994591, 66.60346600605763001, -51.61716770535109333 ) ) ;
#158237=CARTESIAN_POINT ( 'NONE',  ( -17.78241384942737113, 65.14442424719348423, -46.27214515699470354 ) ) ;
#158505=CARTESIAN_POINT ( 'NONE',  ( 20.99999999999999645, 66.25000000001162448, -60.27310748452439526 ) ) ;
#158524=CARTESIAN_POINT ( 'NONE',  ( -12.25000000000000178, 66.65000000001154490, -53.00453852712173841 ) ) ;
#158551=CARTESIAN_POINT ( 'NONE',  ( 18.39999999999999503, 70.35000000001159037, -56.87310748452436115 ) ) ;
#159293=CARTESIAN_POINT ( 'NONE',  ( -23.25000000000000355, 70.35000000001153353, -48.67310748452436542 ) ) ;
#159313=ORIENTED_EDGE ( 'NONE', *, *, #196238, .T. ) ;
#159357=DIRECTION ( 'NONE',  ( 0.000000000000000000, -6.982962677686266711E-15, 1.000000000000000000 ) ) ;
#159489=EDGE_CURVE ( 'NONE', #176630, #45783, #73013, .T. ) ;
#159803=ORIENTED_EDGE ( 'NONE', *, *, #229422, .T. ) ;
#159915=DIRECTION ( 'NONE',  ( -0.000000000000000000, -6.982962677686266711E-15, 1.000000000000000000 ) ) ;
#160198=VECTOR ( 'NONE', #254660, 999.9999999999998863 ) ;
#160249=VERTEX_POINT ( 'NONE', #110185 ) ;
#160330=CARTESIAN_POINT ( 'NONE',  ( -16.81744102076749314, 66.05000000001157900, -56.87310748452438958 ) ) ;
#160536=LINE ( 'NONE', #63977, #138399 ) ;
#160689=CARTESIAN_POINT ( 'NONE',  ( -16.88783316861822215, 66.05000000001157900, -56.77084344254470949 ) ) ;
#160796=LINE ( 'NONE', #223288, #72185 ) ;
#160961=CIRCLE ( 'NONE', #202634, 0.09999999999999516220 ) ;
#160998=CARTESIAN_POINT ( 'NONE',  ( -16.92507428761700083, 66.05000000001153637, -48.73650494414594192 ) ) ;
#161007=CARTESIAN_POINT ( 'NONE',  ( -16.92973740335341404, 66.00749618554429787, -56.92916651972676334 ) ) ;
#161108=CARTESIAN_POINT ( 'NONE',  ( -16.93658211146646408, 66.00589133767039129, -56.92740255448007503 ) ) ;
#161378=CARTESIAN_POINT ( 'NONE',  ( 23.24999999999999645, 67.17743825834511995, -48.67310748452439384 ) ) ;
#161385=CARTESIAN_POINT ( 'NONE',  ( -16.27683809663751191, 66.65000000001160174, -56.97310748452439100 ) ) ;
#161489=B_SPLINE_CURVE_WITH_KNOTS ( 'NONE', 3,
 ( #49289, #132694, #11469, #212240, #188801, #127551, #72745, #230508, #152273, #207096, #229228, #50550, #70171 ),
 .UNSPECIFIED., .F., .F.,
 ( 4, 3, 3, 3, 4 ),
 ( -3.224855718277970714E-06, 0.000000000000000000, 6.199515528666914038E-06, 4.034952380127174165E-05, 7.452715123699336041E-05 ),
 .UNSPECIFIED. ) ;
#161684=ORIENTED_EDGE ( 'NONE', *, *, #50005, .T. ) ;
#161961=CARTESIAN_POINT ( 'NONE',  ( -16.77308656112215601, 66.05000000001157900, -56.87291429282210942 ) ) ;
#162023=FACE_OUTER_BOUND ( 'NONE', #15577, .T. ) ;
#162065=DIRECTION ( 'NONE',  ( -0.000000000000000000, -6.982962677686266711E-15, 1.000000000000000000 ) ) ;
#162156=ORIENTED_EDGE ( 'NONE', *, *, #253073, .F. ) ;
#162196=VERTEX_POINT ( 'NONE', #228983 ) ;
#162463=ORIENTED_EDGE ( 'NONE', *, *, #77842, .T. ) ;
#162499=DIRECTION ( 'NONE',  ( 0.7071067811865456854, 0.7071067811865493491, 4.937700262164544098E-15 ) ) ;
#162651=DIRECTION ( 'NONE',  ( -1.020425574104004196E-15, -6.982962677686266711E-15, 1.000000000000000000 ) ) ;
#162702=CARTESIAN_POINT ( 'NONE',  ( -14.00000000000000178, 66.15000000001155911, -52.77310748452439526 ) ) ;
#162884=CARTESIAN_POINT ( 'NONE',  ( -23.25000000000000355, 70.35000000001160458, -60.27310748452436684 ) ) ;
#162922=CARTESIAN_POINT ( 'NONE',  ( -18.40000000000000213, 64.52683809664910086, -56.91452884076171159 ) ) ;
#163085=EDGE_LOOP ( 'NONE', ( #101773, #92406, #66931, #9238, #232328, #71462 ) ) ;
#163234=CARTESIAN_POINT ( 'NONE',  ( -16.93710578446435733, 66.05000000001157900, -56.60430350072524419 ) ) ;
#163393=CARTESIAN_POINT ( 'NONE',  ( -16.92973740335365562, 66.00749618554431208, -48.61704844932231850 ) ) ;
#163553=AXIS2_PLACEMENT_3D ( 'NONE', #162702, #3605, #4863 ) ;
#163728=DIRECTION ( 'NONE',  ( -1.073024830501117725E-15, 6.982962677686266711E-15, -1.000000000000000000 ) ) ;
#163737=PRODUCT_DEFINITION_SHAPE ( 'NONE', 'NONE',  #21371 ) ;
#163915=DIRECTION ( 'NONE',  ( 1.000000000000000000, 7.492892343619937423E-30, -1.073024830501117725E-15 ) ) ;
#163978=VERTEX_POINT ( 'NONE', #62916 ) ;
#164080=DIRECTION ( 'NONE',  ( 0.5932847527679310229, 0.8049926720990042694, 6.257843056355992909E-15 ) ) ;
#164120=CARTESIAN_POINT ( 'NONE',  ( -16.82542659449985223, 66.06550010858410360, -48.76774308455063078 ) ) ;
#164151=ORIENTED_EDGE ( 'NONE', *, *, #30392, .F. ) ;
#164189=CARTESIAN_POINT ( 'NONE',  ( 18.39999999999999503, 64.52683809664910086, -56.87310748452440379 ) ) ;
#164233=CARTESIAN_POINT ( 'NONE',  ( -18.34804628011471195, 64.52683809664921455, -60.27310748452440947 ) ) ;
#164238=DIRECTION ( 'NONE',  ( 1.000000000000000000, 0.000000000000000000, 0.000000000000000000 ) ) ;
#164282=VECTOR ( 'NONE', #163915, 1000.000000000000000 ) ;
#164366=EDGE_LOOP ( 'NONE', ( #30506, #181419 ) ) ;
#164675=CARTESIAN_POINT ( 'NONE',  ( -16.92778301347278003, 65.99905508317625902, -48.59458937655572441 ) ) ;
#164743=VECTOR ( 'NONE', #143069, 1000.000000000000000 ) ;
#164964=ORIENTED_EDGE ( 'NONE', *, *, #180357, .T. ) ;
#164993=EDGE_CURVE ( 'NONE', #16468, #212431, #75716, .T. ) ;
#165153=EDGE_CURVE ( 'NONE', #188280, #19024, #50915, .T. ) ;
#165305=CARTESIAN_POINT ( 'NONE',  ( -17.22767730083113946, 65.65075578754417052, -58.16553617509497087 ) ) ;
#165401=CARTESIAN_POINT ( 'NONE',  ( -16.97683810757273193, 66.05000000001153637, -49.28668419698479397 ) ) ;
#165480=FACE_OUTER_BOUND ( 'NONE', #197606, .T. ) ;
#165528=CARTESIAN_POINT ( 'NONE',  ( 13.99999999999999822, 66.15000000001155911, -52.77310748452440237 ) ) ;
#165632=EDGE_CURVE ( 'NONE', #202498, #249506, #201689, .T. ) ;
#165650=ORIENTED_EDGE ( 'NONE', *, *, #201933, .F. ) ;
#165932=CARTESIAN_POINT ( 'NONE',  ( -21.65000000000000213, 68.75000000001161027, -60.27310748452437394 ) ) ;
#166032=LINE ( 'NONE', #23948, #31246 ) ;
#166118=VECTOR ( 'NONE', #239893, 1000.000000000000000 ) ;
#166146=B_SPLINE_CURVE_WITH_KNOTS ( 'NONE', 3,
 ( #214762, #131376, #12748, #255123, #195239, #71430, #152258, #156113, #31037, #212224, #231781, #250048, #113104, #150952, #110527, #32314, #133938, #111830, #191391, #92242, #251316, #192651, #252600, #74016, #54409, #99924 ),
 .UNSPECIFIED., .F., .F.,
 ( 4, 2, 2, 2, 2, 2, 2, 2, 2, 2, 2, 2, 4 ),
 ( 0.005476422646581343909, 0.006160811967703539241, 0.006845201288825734573, 0.007187395949386840913, 0.007529590609947948120, 0.007871785270509055327, 0.008213979931070161666, 0.008556174591631268006, 0.008898369252192374346, 0.009240563912753480685, 0.009582758573314588760, 0.01026714789443680838, 0.01095153721555902800 ),
 .UNSPECIFIED. ) ;
#166521=DIRECTION ( 'NONE',  ( 1.000000000000000000, -7.125593699324843413E-30, 1.020425574104004196E-15 ) ) ;
#166688=AXIS2_PLACEMENT_3D ( 'NONE', #75883, #177594, #138395 ) ;
#166890=FACE_OUTER_BOUND ( 'NONE', #155754, .T. ) ;
#167004=AXIS2_PLACEMENT_3D ( 'NONE', #84694, #83420, #221658 ) ;
#167304=AXIS2_PLACEMENT_3D ( 'NONE', #52172, #33956, #131722 ) ;
#167353=VECTOR ( 'NONE', #34659, 1000.000000000000000 ) ;
#167450=CARTESIAN_POINT ( 'NONE',  ( -16.86578989773640913, 66.01519019875270544, -48.55844259790215744 ) ) ;
#167520=EDGE_CURVE ( 'NONE', #256608, #209103, #112775, .T. ) ;
#167525=DIRECTION ( 'NONE',  ( 0.000000000000000000, -1.000000000000000000, -6.982962677686266711E-15 ) ) ;
#167934=ORIENTED_EDGE ( 'NONE', *, *, #164993, .F. ) ;
#168202=AXIS2_PLACEMENT_3D ( 'NONE', #111922, #70243, #14108 ) ;
#168336=CARTESIAN_POINT ( 'NONE',  ( -16.94107738177415712, 65.98576071487495653, -56.97310748452439810 ) ) ;
#168584=ADVANCED_FACE ( 'NONE', ( #235626 ), #60836, .F. ) ;
#168703=AXIS2_PLACEMENT_3D ( 'NONE', #132838, #57107, #54562 ) ;
#168765=CARTESIAN_POINT ( 'NONE',  ( -16.87786941232801041, 66.04184528586654324, -48.64592168473038214 ) ) ;
#168901=EDGE_CURVE ( 'NONE', #245959, #76969, #47053, .T. ) ;
#168940=DIRECTION ( 'NONE',  ( 1.652117596168391700E-15, -1.000000000000000000, -6.982962677686266711E-15 ) ) ;
#169122=EDGE_LOOP ( 'NONE', ( #65573, #208288, #84162, #205860, #88324 ) ) ;
#169185=CARTESIAN_POINT ( 'NONE',  ( -14.56336952470180002, 66.55335465531629779, -51.11230102842421275 ) ) ;
#169742=CARTESIAN_POINT ( 'NONE',  ( -16.97683809663752186, 66.05000000001155058, -49.42547150272071121 ) ) ;
#169982=PLANE ( 'NONE',  #34715 ) ;
#169987=ORIENTED_EDGE ( 'NONE', *, *, #188332, .T. ) ;
#170112=CARTESIAN_POINT ( 'NONE',  ( -18.40000000000000213, 70.35000000001159037, -56.87310748452436115 ) ) ;
#170365=ORIENTED_EDGE ( 'NONE', *, *, #104652, .T. ) ;
#170398=VECTOR ( 'NONE', #200107, 1000.000000000000000 ) ;
#170469=AXIS2_PLACEMENT_3D ( 'NONE', #6889, #186832, #27778 ) ;
#170988=AXIS2_PLACEMENT_3D ( 'NONE', #190, #103133, #182711 ) ;
#171092=DIRECTION ( 'NONE',  ( 0.000000000000000000, -6.982962677686266711E-15, 1.000000000000000000 ) ) ;
#171224=FILL_AREA_STYLE_COLOUR ( '', #81677 ) ;
#171588=EDGE_CURVE ( 'NONE', #250894, #13299, #133311, .T. ) ;
#171674=ORIENTED_EDGE ( 'NONE', *, *, #200150, .T. ) ;
#171930=CARTESIAN_POINT ( 'NONE',  ( -16.87036670365549895, 65.91505003675629837, -56.97310748452439810 ) ) ;
#172145=ORIENTED_EDGE ( 'NONE', *, *, #253073, .T. ) ;
#172216=CARTESIAN_POINT ( 'NONE',  ( -16.89020380669786903, 66.05000000001157900, -56.76569633641382495 ) ) ;
#172296=LINE ( 'NONE', #109689, #180051 ) ;
#172358=ORIENTED_EDGE ( 'NONE', *, *, #188461, .F. ) ;
#172512=( LENGTH_UNIT ( ) NAMED_UNIT ( * ) SI_UNIT ( .MILLI., .METRE. ) );
#172990=B_SPLINE_CURVE_WITH_KNOTS ( 'NONE', 3,
 ( #41300, #135215, #157405, #136493, #140353, #60813, #219903, #36152, #235604, #236897 ),
 .UNSPECIFIED., .F., .F.,
 ( 4, 3, 3, 4 ),
 ( 1.887726692324194669E-15, 3.877043166999659889E-05, 7.336897548475921900E-05, 7.659383120240320164E-05 ),
 .UNSPECIFIED. ) ;
#173299=DIRECTION ( 'NONE',  ( -0.7071067811865487940, -0.7071067811865463515, -4.216150419019404490E-15 ) ) ;
#173338=EDGE_CURVE ( 'NONE', #145079, #243577, #160961, .T. ) ;
#173503=FACE_OUTER_BOUND ( 'NONE', #196799, .T. ) ;
#173507=ORIENTED_EDGE ( 'NONE', *, *, #117492, .F. ) ;
#173912=CARTESIAN_POINT ( 'NONE',  ( 15.66039659514495419, 66.63925083009641526, -52.20853734391710077 ) ) ;
#174011=ORIENTED_EDGE ( 'NONE', *, *, #192762, .T. ) ;
#174232=CARTESIAN_POINT ( 'NONE',  ( -16.89268316805465986, 66.04827818676933759, -48.66735500597884823 ) ) ;
#174529=CARTESIAN_POINT ( 'NONE',  ( -16.98495255085916611, 65.99443563401675306, -48.65772469074489948 ) ) ;
#174959=ORIENTED_EDGE ( 'NONE', *, *, #72927, .T. ) ;
#175039=CARTESIAN_POINT ( 'NONE',  ( 21.13736287352038445, 67.95335762362756782, -56.87310748452437537 ) ) ;
#175076=SHAPE_REPRESENTATION_RELATIONSHIP ( 'NONE' , 'NONE' ,  #100031, #178764 ) ;
#175196=CARTESIAN_POINT ( 'NONE',  ( 12.48201962039795809, 66.62334006147798959, -51.89491493630711716 ) ) ;
#175218=CARTESIAN_POINT ( 'NONE',  ( 15.48841904831874849, 67.43841904833035983, -56.87310748452438247 ) ) ;
#175465=ORIENTED_EDGE ( 'NONE', *, *, #1595, .T. ) ;
#175567=DIRECTION ( 'NONE',  ( -1.000000000000000000, -1.652117596168391700E-15, -1.153667551319263085E-29 ) ) ;
#175650=CARTESIAN_POINT ( 'NONE',  ( -16.87036670365548474, 65.91505003675624152, -48.57310748452439952 ) ) ;
#175790=UNCERTAINTY_MEASURE_WITH_UNIT (LENGTH_MEASURE( 1.000000000000000082E-05 ), #56340, 'distance_accuracy_value', 'NONE');
#175948=CARTESIAN_POINT ( 'NONE',  ( -33.72168855820452649, 64.52683809664901560, -45.27310748452439526 ) ) ;
#175987=CARTESIAN_POINT ( 'NONE',  ( -16.85939681242906119, 66.09477481408619326, -48.98318552933291414 ) ) ;
#175988=ORIENTED_EDGE ( 'NONE', *, *, #14079, .F. ) ;
#176029=LINE ( 'NONE', #215130, #64568 ) ;
#176347=EDGE_CURVE ( 'NONE', #205644, #19990, #783, .T. ) ;
#176580=VERTEX_POINT ( 'NONE', #175039 ) ;
#176630=VERTEX_POINT ( 'NONE', #159293 ) ;
#176774=DIRECTION ( 'NONE',  ( -0.5932847527679298016, -0.8049926720990051576, -5.621233785078291429E-15 ) ) ;
#176866=CARTESIAN_POINT ( 'NONE',  ( -17.04295772865458858, 65.97510057475003009, -48.67310748452439384 ) ) ;
#176980=AXIS2_PLACEMENT_3D ( 'NONE', #252800, #12949, #228130 ) ;
#177001=CIRCLE ( 'NONE', #43688, 0.5000000000000004441 ) ;
#177354=SURFACE_STYLE_FILL_AREA ( #116073 ) ;
#177594=DIRECTION ( 'NONE',  ( 1.186688945009009831E-16, 1.000000000000000000, 6.982962677686266711E-15 ) ) ;
#177652=LINE ( 'NONE', #237599, #248623 ) ;
#177744=CARTESIAN_POINT ( 'NONE',  ( 14.22916352759893321, 66.54258906972138732, -51.02319157577811382 ) ) ;
#178083=CARTESIAN_POINT ( 'NONE',  ( -12.84409460144754078, 66.58931770574362474, -54.09196404257613722 ) ) ;
#178091=ORIENTED_EDGE ( 'NONE', *, *, #72833, .T. ) ;
#178263=CARTESIAN_POINT ( 'NONE',  ( 23.24999999999999645, 64.25000000001161027, -60.27310748452440947 ) ) ;
#178764=ADVANCED_BREP_SHAPE_REPRESENTATION ( '', ( #110136, #2425 ), #77591 ) ;
#178924=ADVANCED_FACE ( 'NONE', ( #98366, #59240, #39759 ), #20176, .T. ) ;
#179266=DIRECTION ( 'NONE',  ( 1.000000000000000000, 0.000000000000000000, 0.000000000000000000 ) ) ;
#179321=CARTESIAN_POINT ( 'NONE',  ( 13.99999999999999822, 66.15000000001155911, -52.77310748452440237 ) ) ;
#179443=DIRECTION ( 'NONE',  ( 0.000000000000000000, 6.982962677686266711E-15, -1.000000000000000000 ) ) ;
#179520=FACE_OUTER_BOUND ( 'NONE', #242779, .T. ) ;
#179532=CARTESIAN_POINT ( 'NONE',  ( -16.89268316805466341, 66.04827818676939444, -56.87885996306994230 ) ) ;
#179752=CARTESIAN_POINT ( 'NONE',  ( -16.94445028196808778, 66.00793639031384430, -56.91577730610593733 ) ) ;
#179902=CYLINDRICAL_SURFACE ( 'NONE', #216120, 0.09999999999999939493 ) ;
#180030=CARTESIAN_POINT ( 'NONE',  ( 20.73486653747090003, 68.75000000001149658, -48.67310748452437963 ) ) ;
#180051=VECTOR ( 'NONE', #113556, 999.9999999999998863 ) ;
#180138=AXIS2_PLACEMENT_3D ( 'NONE', #257883, #256597, #98824 ) ;
#180155=DIRECTION ( 'NONE',  ( -1.652117596168391700E-15, 1.000000000000000000, 6.982962677686266711E-15 ) ) ;
#180231=CARTESIAN_POINT ( 'NONE',  ( -16.87683809663750623, 66.05000000001157900, -56.12074346632790878 ) ) ;
#180347=VERTEX_POINT ( 'NONE', #68184 ) ;
#180357=EDGE_CURVE ( 'NONE', #120974, #160249, #227245, .T. ) ;
#180663=CARTESIAN_POINT ( 'NONE',  ( -18.40000000000000213, 64.25000000001159606, -56.87310748452440379 ) ) ;
#180871=CARTESIAN_POINT ( 'NONE',  ( -21.65000000000000213, 65.95000000001152785, -48.67310748452439384 ) ) ;
#180975=CARTESIAN_POINT ( 'NONE',  ( 18.39999999999999147, 67.17743825834520521, -60.27310748452438816 ) ) ;
#181193=VECTOR ( 'NONE', #137656, 1000.000000000000000 ) ;
#181201=CARTESIAN_POINT ( 'NONE',  ( -14.00000000000000178, 66.15000000001155911, -52.77310748452439526 ) ) ;
#181356=CIRCLE ( 'NONE', #68935, 0.9000000000000014655 ) ;
#181419=ORIENTED_EDGE ( 'NONE', *, *, #14079, .T. ) ;
#181484=CARTESIAN_POINT ( 'NONE',  ( 20.27550659511089037, 66.78395627750268204, -48.67310748452439384 ) ) ;
#181522=CARTESIAN_POINT ( 'NONE',  ( -16.84981964351482731, 66.08268176591292331, -56.65350587050463815 ) ) ;
#181669=VERTEX_POINT ( 'NONE', #250401 ) ;
#182241=ORIENTED_EDGE ( 'NONE', *, *, #188461, .T. ) ;
#182360=EDGE_CURVE ( 'NONE', #148974, #57410, #14077, .T. ) ;
#182458=AXIS2_PLACEMENT_3D ( 'NONE', #81515, #78952, #101057 ) ;
#182473=DIRECTION ( 'NONE',  ( 0.000000000000000000, -6.982962677686266711E-15, 1.000000000000000000 ) ) ;
#182479=CARTESIAN_POINT ( 'NONE',  ( -18.40000000000000213, 64.52683809664910086, -56.97310748452440521 ) ) ;
#182711=DIRECTION ( 'NONE',  ( -1.020425574104004196E-15, 6.982962677686266711E-15, -1.000000000000000000 ) ) ;
#182807=CARTESIAN_POINT ( 'NONE',  ( -16.87401514999235275, 66.05000000001157900, -56.80312547705646153 ) ) ;
#182909=CARTESIAN_POINT ( 'NONE',  ( -16.88853107394619357, 66.04912151666452758, -48.67017113763215974 ) ) ;
#182946=CARTESIAN_POINT ( 'NONE',  ( -17.29158576265543346, 65.63525233399359138, -47.44034923973222106 ) ) ;
#182964=CARTESIAN_POINT ( 'NONE',  ( -16.91256925476570672, 66.01426884188333588, -48.55546499551912376 ) ) ;
#183139=ORIENTED_EDGE ( 'NONE', *, *, #72860, .T. ) ;
#183442=CARTESIAN_POINT ( 'NONE',  ( -18.40000000000000213, 64.51332499825382172, -45.27310748452440947 ) ) ;
#183480=LINE ( 'NONE', #84309, #164282 ) ;
#183654=CARTESIAN_POINT ( 'NONE',  ( -15.75000000000000355, 66.65000000001155911, -52.77310748452439526 ) ) ;
#183786=CARTESIAN_POINT ( 'NONE',  ( -18.35235881385853318, 64.52658099229870459, -60.27310748452440947 ) ) ;
#183840=CARTESIAN_POINT ( 'NONE',  ( 15.74999999999999645, 66.15000000001155911, -52.77310748452440237 ) ) ;
#184063=CARTESIAN_POINT ( 'NONE',  ( -16.84793658983426923, 66.05000000001159322, -56.78946080671413199 ) ) ;
#184257=DIRECTION ( 'NONE',  ( -1.000000000000000000, 7.492892343619937423E-30, -1.073024830501117725E-15 ) ) ;
#184477=CARTESIAN_POINT ( 'NONE',  ( 20.73486653747088937, 68.25000000001155342, -56.87310748452437537 ) ) ;
#184604=CARTESIAN_POINT ( 'NONE',  ( -15.55912972643740488, 67.50912972644894694, -48.67310748452438673 ) ) ;
#184608=EDGE_LOOP ( 'NONE', ( #121122, #159803, #215845, #152158 ) ) ;
#185539=DIRECTION ( 'NONE',  ( 0.000000000000000000, -1.000000000000000000, -6.982962677686266711E-15 ) ) ;
#185769=ORIENTED_EDGE ( 'NONE', *, *, #123615, .F. ) ;
#186149=CARTESIAN_POINT ( 'NONE',  ( -12.25000000000000000, 66.65000000001154490, -52.65736431725047595 ) ) ;
#186210=LINE ( 'NONE', #247455, #67819 ) ;
#186420=LINE ( 'NONE', #241258, #6778 ) ;
#186530=LINE ( 'NONE', #26175, #58072 ) ;
#186608=CARTESIAN_POINT ( 'NONE',  ( -16.91049119928364419, 66.05000000001160743, -56.90482787771522766 ) ) ;
#186815=FACE_OUTER_BOUND ( 'NONE', #257285, .T. ) ;
#186832=DIRECTION ( 'NONE',  ( 1.000000000000000000, 0.000000000000000000, 0.000000000000000000 ) ) ;
#187081=DIRECTION ( 'NONE',  ( -1.000000000000000000, 0.000000000000000000, 0.000000000000000000 ) ) ;
#187206=AXIS2_PLACEMENT_3D ( 'NONE', #241951, #2043, #64592 ) ;
#187540=DIRECTION ( 'NONE',  ( 1.000000000000000000, 0.000000000000000000, 0.000000000000000000 ) ) ;
#187548=CARTESIAN_POINT ( 'NONE',  ( -16.86379686415369861, 66.02478224075841240, -56.95649737361467402 ) ) ;
#187658=CARTESIAN_POINT ( 'NONE',  ( -18.40000000000000213, 64.51332499825393541, -60.27310748452440947 ) ) ;
#187671=VERTEX_POINT ( 'NONE', #101923 ) ;
#187792=EDGE_CURVE ( 'NONE', #5771, #63364, #45829, .T. ) ;
#188077=FACE_OUTER_BOUND ( 'NONE', #81799, .T. ) ;
#188216=ORIENTED_EDGE ( 'NONE', *, *, #76576, .F. ) ;
#188280=VERTEX_POINT ( 'NONE', #77568 ) ;
#188332=EDGE_CURVE ( 'NONE', #145079, #65805, #253650, .T. ) ;
#188434=EDGE_CURVE ( 'NONE', #76969, #112394, #45553, .T. ) ;
#188461=EDGE_CURVE ( 'NONE', #19990, #160249, #181356, .T. ) ;
#188740=DIRECTION ( 'NONE',  ( 0.000000000000000000, -1.000000000000000000, -6.982962677686266711E-15 ) ) ;
#188801=CARTESIAN_POINT ( 'NONE',  ( -16.94165728009537020, 66.01213024408774288, -48.63205247601419501 ) ) ;
#188964=LINE ( 'NONE', #10340, #241051 ) ;
#189033=CARTESIAN_POINT ( 'NONE',  ( -18.34374000495060386, 64.52683809664912928, -60.27310748452440947 ) ) ;
#189051=B_SPLINE_CURVE_WITH_KNOTS ( 'NONE', 3,
 ( #31403, #190467, #11834, #91354, #52194, #92604, #172216, #232151, #41660, #160330 ),
 .UNSPECIFIED., .F., .F.,
 ( 4, 2, 2, 2, 4 ),
 ( 0.000000000000000000, 0.0003916577441626807577, 0.0005874866162440115685, 0.0006854010522846854577, 0.0007833154883253592386 ),
 .UNSPECIFIED. ) ;
#189149=AXIS2_PLACEMENT_3D ( 'NONE', #1626, #84998, #47161 ) ;
#189171=B_SPLINE_CURVE_WITH_KNOTS ( 'NONE', 3,
 ( #231800, #33634, #14034, #187548, #130106, #209654, #218617, #235620, #55669, #179532 ),
 .UNSPECIFIED., .F., .F.,
 ( 4, 3, 3, 4 ),
 ( 0.000000000000000000, 4.874959354402235258E-05, 9.785140065120555329E-05, 0.0001360444631936037936 ),
 .UNSPECIFIED. ) ;
#189292=CARTESIAN_POINT ( 'NONE',  ( -23.25000000000000355, 64.25000000001151079, -45.27310748452440947 ) ) ;
#189323=VECTOR ( 'NONE', #157188, 1000.000000000000000 ) ;
#189376=CARTESIAN_POINT ( 'NONE',  ( -18.40000000000000213, 64.52683809664901560, -45.34905355133235361 ) ) ;
#189657=DIRECTION ( 'NONE',  ( -0.000000000000000000, -6.982962677686266711E-15, 1.000000000000000000 ) ) ;
#189858=CARTESIAN_POINT ( 'NONE',  ( -17.04761207306819770, 65.97354912661380411, -56.87310748452438247 ) ) ;
#189943=VECTOR ( 'NONE', #59367, 1000.000000000000000 ) ;
#190074=VERTEX_POINT ( 'NONE', #150169 ) ;
#190467=CARTESIAN_POINT ( 'NONE',  ( -16.97683809663753252, 66.05000000001157900, -56.25158271585445391 ) ) ;
#190471=FACE_OUTER_BOUND ( 'NONE', #197990, .T. ) ;
#190730=DIRECTION ( 'NONE',  ( -0.000000000000000000, -6.982962677686266711E-15, 1.000000000000000000 ) ) ;
#191221=STYLED_ITEM ( 'NONE', ( #39116 ), #110136 ) ;
#191369=EDGE_CURVE ( 'NONE', #214271, #208794, #236769, .T. ) ;
#191377=LINE ( 'NONE', #17826, #71182 ) ;
#191391=CARTESIAN_POINT ( 'NONE',  ( 14.87567385445976953, 66.56923500458921694, -54.29257008977393184 ) ) ;
#191526=CARTESIAN_POINT ( 'NONE',  ( -18.40000000000000213, 64.51332499825393541, -60.27310748452440947 ) ) ;
#191532=CARTESIAN_POINT ( 'NONE',  ( -21.65000000000000213, 68.75000000001159606, -56.87310748452436826 ) ) ;
#191677=ORIENTED_EDGE ( 'NONE', *, *, #12279, .T. ) ;
#191764=CARTESIAN_POINT ( 'NONE',  ( -17.11825945287482753, 66.05000000001159322, -56.77310748452439526 ) ) ;
#192036=ORIENTED_EDGE ( 'NONE', *, *, #140570, .T. ) ;
#192135=ORIENTED_EDGE ( 'NONE', *, *, #1863, .T. ) ;
#192146=DIRECTION ( 'NONE',  ( 0.000000000000000000, 0.000000000000000000, -1.000000000000000000 ) ) ;
#192279=CARTESIAN_POINT ( 'NONE',  ( -18.39999999999999858, 64.52683809664912928, -60.19716141771643692 ) ) ;
#192335=CARTESIAN_POINT ( 'NONE',  ( -16.77732147278574715, 66.05403306743814085, -56.85959872764858147 ) ) ;
#192345=EDGE_CURVE ( 'NONE', #46675, #76969, #106006, .T. ) ;
#192363=EDGE_LOOP ( 'NONE', ( #246266, #230370, #213994 ) ) ;
#192508=LINE ( 'NONE', #11305, #244268 ) ;
#192615=ADVANCED_FACE ( 'NONE', ( #78135 ), #145305, .F. ) ;
#192651=CARTESIAN_POINT ( 'NONE',  ( 15.39793903038208001, 66.61031399435591993, -53.85026397817310340 ) ) ;
#192762=EDGE_CURVE ( 'NONE', #98576, #14611, #161489, .T. ) ;
#192763=EDGE_CURVE ( 'NONE', #249506, #187671, #189171, .T. ) ;
#192855=PLANE ( 'NONE',  #176980 ) ;
#193047=DIRECTION ( 'NONE',  ( -1.073024830501117725E-15, 6.982962677686266711E-15, -1.000000000000000000 ) ) ;
#193249=CARTESIAN_POINT ( 'NONE',  ( -20.65000000000000568, 68.75000000001153921, -48.67310748452437252 ) ) ;
#193282=AXIS2_PLACEMENT_3D ( 'NONE', #137036, #99164, #20968 ) ;
#193477=ORIENTED_EDGE ( 'NONE', *, *, #29972, .F. ) ;
#193491=ORIENTED_EDGE ( 'NONE', *, *, #246576, .T. ) ;
#193563=VECTOR ( 'NONE', #252033, 1000.000000000000000 ) ;
#193810=CARTESIAN_POINT ( 'NONE',  ( -18.40000000000000213, 70.35000000001151932, -45.27310748452435973 ) ) ;
#193950=ORIENTED_EDGE ( 'NONE', *, *, #168901, .F. ) ;
#194170=( GEOMETRIC_REPRESENTATION_CONTEXT ( 3 ) GLOBAL_UNCERTAINTY_ASSIGNED_CONTEXT ( ( #152387 ) ) GLOBAL_UNIT_ASSIGNED_CONTEXT ( ( #172512, #91638, #113757 ) ) REPRESENTATION_CONTEXT ( 'NONE', 'WORKASPACE' ) );
#194323=DIRECTION ( 'NONE',  ( 1.186688945009010077E-16, 1.000000000000000000, 6.982962677686266711E-15 ) ) ;
#194655=ORIENTED_EDGE ( 'NONE', *, *, #241499, .F. ) ;
#194716=ORIENTED_EDGE ( 'NONE', *, *, #102781, .T. ) ;
#194731=CARTESIAN_POINT ( 'NONE',  ( -18.40000000000000568, 64.58541674041173053, -48.67310748452441516 ) ) ;
#194736=CARTESIAN_POINT ( 'NONE',  ( 12.26145404764308111, 66.64858632091014101, -52.54276391697543147 ) ) ;
#194758=CARTESIAN_POINT ( 'NONE',  ( 16.87683809663749557, 66.05000000001155058, -48.67310748452439384 ) ) ;
#194919=CARTESIAN_POINT ( 'NONE',  ( -16.77902162784673834, 66.05358074280371738, -56.86111624045504698 ) ) ;
#195116=CARTESIAN_POINT ( 'NONE',  ( 22.88900146558018989, 67.29609520889876251, -56.87310748452437537 ) ) ;
#195239=CARTESIAN_POINT ( 'NONE',  ( 12.60053434924910221, 66.61046543766484263, -53.84829818013444225 ) ) ;
#195342=CARTESIAN_POINT ( 'NONE',  ( -16.94445028196807002, 66.00793639031378746, -48.63043766294283898 ) ) ;
#195599=CARTESIAN_POINT ( 'NONE',  ( 18.39999999999999503, 70.35000000001151932, -45.27310748452435973 ) ) ;
#195704=DIRECTION ( 'NONE',  ( 1.020425574104004196E-15, -6.982962677686266711E-15, 1.000000000000000000 ) ) ;
#195892=PRESENTATION_STYLE_ASSIGNMENT (( #231174 ) ) ;
#196007=CARTESIAN_POINT ( 'NONE',  ( 13.12229106158772929, 66.56936289831479314, -51.25484686646344556 ) ) ;
#196238=EDGE_CURVE ( 'NONE', #48902, #91508, #43920, .T. ) ;
#196241=EDGE_CURVE ( 'NONE', #208794, #253814, #91928, .T. ) ;
#196345=CARTESIAN_POINT ( 'NONE',  ( -14.00000000000000178, 66.15000000001155911, -52.77310748452439526 ) ) ;
#196493=CARTESIAN_POINT ( 'NONE',  ( -16.93211319090181632, 66.00001321885403627, -48.60060198525133046 ) ) ;
#196603=EDGE_CURVE ( 'NONE', #14611, #243577, #125619, .T. ) ;
#196693=ADVANCED_FACE ( 'NONE', ( #90437 ), #52600, .T. ) ;
#196722=AXIS2_PLACEMENT_3D ( 'NONE', #178263, #56969, #257706 ) ;
#196738=LINE ( 'NONE', #97617, #77085 ) ;
#196799=EDGE_LOOP ( 'NONE', ( #173507, #245613, #211770, #11932 ) ) ;
#197012=CARTESIAN_POINT ( 'NONE',  ( 18.54999999999999716, 52.34166666667822199, -52.77310748452448763 ) ) ;
#197034=AXIS2_PLACEMENT_3D ( 'NONE', #193810, #33489, #72594 ) ;
#197047=VERTEX_POINT ( 'NONE', #206249 ) ;
#197124=FACE_OUTER_BOUND ( 'NONE', #107257, .T. ) ;
#197216=AXIS2_PLACEMENT_3D ( 'NONE', #213273, #13802, #94609 ) ;
#197274=CARTESIAN_POINT ( 'NONE',  ( 15.73863059295127798, 66.64859682586990175, -52.54357704768591475 ) ) ;
#197342=DIRECTION ( 'NONE',  ( 0.000000000000000000, -6.982962677686266711E-15, 1.000000000000000000 ) ) ;
#197374=ORIENTED_EDGE ( 'NONE', *, *, #14243, .F. ) ;
#197495=ORIENTED_EDGE ( 'NONE', *, *, #56548, .T. ) ;
#197606=EDGE_LOOP ( 'NONE', ( #36371, #175465 ) ) ;
#197615=CARTESIAN_POINT ( 'NONE',  ( -14.87779219673429054, 66.56936653093875123, -54.29134168970030316 ) ) ;
#197641=FACE_OUTER_BOUND ( 'NONE', #163085, .T. ) ;
#197730=AXIS2_PLACEMENT_3D ( 'NONE', #197012, #254408, #14571 ) ;
#197990=EDGE_LOOP ( 'NONE', ( #17187, #145074, #66219, #94077, #147064 ) ) ;
#198049=EDGE_CURVE ( 'NONE', #176580, #180347, #176029, .T. ) ;
#198088=CARTESIAN_POINT ( 'NONE',  ( -16.87683809663752399, 66.15000000001153069, -49.42547150272069700 ) ) ;
#198158=( LENGTH_UNIT ( ) NAMED_UNIT ( * ) SI_UNIT ( .MILLI., .METRE. ) );
#198286=PLANE ( 'NONE',  #193282 ) ;
#198439=DIRECTION ( 'NONE',  ( -1.000000000000000000, 0.000000000000000000, 0.000000000000000000 ) ) ;
#198492=CARTESIAN_POINT ( 'NONE',  ( -16.87683809663752399, 66.15000000001160174, -56.12074346632791588 ) ) ;
#198599=CARTESIAN_POINT ( 'NONE',  ( -17.73285935861037288, 65.14201819622032019, -46.26454567474291935 ) ) ;
#198659=VECTOR ( 'NONE', #95716, 1000.000000000000000 ) ;
#198673=AXIS2_PLACEMENT_3D ( 'NONE', #206649, #189657, #231364 ) ;
#198927=DIRECTION ( 'NONE',  ( 0.000000000000000000, -1.000000000000000000, -6.982962677686266711E-15 ) ) ;
#198935=EDGE_CURVE ( 'NONE', #128091, #256608, #158122, .T. ) ;
#198967=EDGE_CURVE ( 'NONE', #99410, #100756, #215028, .T. ) ;
#198993=ORIENTED_EDGE ( 'NONE', *, *, #95635, .T. ) ;
#199344=CARTESIAN_POINT ( 'NONE',  ( -15.55912972643741199, 67.50912972644901799, -56.87310748452438247 ) ) ;
#200107=DIRECTION ( 'NONE',  ( -1.000000000000000000, -0.000000000000000000, -0.000000000000000000 ) ) ;
#200150=EDGE_CURVE ( 'NONE', #139671, #224622, #114066, .T. ) ;
#200179=DIRECTION ( 'NONE',  ( 0.8049926720990051576, -0.5932847527679298016, -4.142885285818778274E-15 ) ) ;
#200200=CARTESIAN_POINT ( 'NONE',  ( -13.77178122865954357, 66.54397173950366096, -54.51190944945868466 ) ) ;
#200258=ORIENTED_EDGE ( 'NONE', *, *, #53915, .F. ) ;
#200639=LINE ( 'NONE', #143210, #114934 ) ;
#200737=DIRECTION ( 'NONE',  ( -1.073024830501117725E-15, -6.982962677686266711E-15, 1.000000000000000000 ) ) ;
#201018=AXIS2_PLACEMENT_3D ( 'NONE', #59000, #85936, #222902 ) ;
#201050=CARTESIAN_POINT ( 'NONE',  ( -16.81453046979148880, 66.06089771857064363, -56.81138096092137602 ) ) ;
#201063=CARTESIAN_POINT ( 'NONE',  ( -16.89935556175704079, 66.05000000001159322, -56.38343112163853021 ) ) ;
#201339=DIRECTION ( 'NONE',  ( -0.000000000000000000, -6.982962677686266711E-15, 1.000000000000000000 ) ) ;
#201419=DIRECTION ( 'NONE',  ( 1.000000000000000000, 0.000000000000000000, 0.000000000000000000 ) ) ;
#201464=CARTESIAN_POINT ( 'NONE',  ( -15.39946565075089779, 66.61046543766484263, -53.84829818013443514 ) ) ;
#201635=AXIS2_PLACEMENT_3D ( 'NONE', #204148, #145465, #129761 ) ;
#201689=( BOUNDED_CURVE ( )  B_SPLINE_CURVE ( 3, ( #189033, #89915, #208612, #249024 ),
 .UNSPECIFIED., .F., .F. ) 
 B_SPLINE_CURVE_WITH_KNOTS ( ( 4, 4 ),
 ( 5.731445031868799056, 5.983100554402348337 ),
 .UNSPECIFIED. ) 
 CURVE ( )  GEOMETRIC_REPRESENTATION_ITEM ( )  RATIONAL_B_SPLINE_CURVE ( ( 1.000000000000000000, 0.9947294176030464508, 0.9947294176030464508, 1.000000000000000000 ) ) 
 REPRESENTATION_ITEM ( '' )  );
#201933=EDGE_CURVE ( 'NONE', #139671, #86511, #136777, .T. ) ;
#201960=CARTESIAN_POINT ( 'NONE',  ( -16.85722902420167202, 66.05000000001153637, -48.78865495829463583 ) ) ;
#202259=PLANE ( 'NONE',  #170988 ) ;
#202333=CARTESIAN_POINT ( 'NONE',  ( -16.83794237512074332, 66.07364077890409249, -56.71956532582543531 ) ) ;
#202498=VERTEX_POINT ( 'NONE', #9797 ) ;
#202634=AXIS2_PLACEMENT_3D ( 'NONE', #175650, #59502, #80349 ) ;
#202753=CIRCLE ( 'NONE', #90318, 14.20833333333333748 ) ;
#203096=EDGE_CURVE ( 'NONE', #187671, #235449, #35748, .T. ) ;
#203638=VECTOR ( 'NONE', #51908, 1000.000000000000000 ) ;
#203786=CARTESIAN_POINT ( 'NONE',  ( -17.05016517656093811, 66.05000000001152216, -48.69580548052332603 ) ) ;
#203960=DIRECTION ( 'NONE',  ( 1.000000000000000000, 0.000000000000000000, 0.000000000000000000 ) ) ;
#204037=( BOUNDED_CURVE ( )  B_SPLINE_CURVE ( 3, ( #139467, #238581, #162922, #182479 ),
 .UNSPECIFIED., .F., .T. ) 
 B_SPLINE_CURVE_WITH_KNOTS ( ( 4, 4 ),
 ( 1.570796326794892339, 3.141592653589784678 ),
 .UNSPECIFIED. ) 
 CURVE ( )  GEOMETRIC_REPRESENTATION_ITEM ( )  RATIONAL_B_SPLINE_CURVE ( ( 1.000000000000000000, 0.8047378541243659367, 0.8047378541243659367, 1.000000000000000000 ) ) 
 REPRESENTATION_ITEM ( '' )  );
#204054=CARTESIAN_POINT ( 'NONE',  ( -21.65000000000000213, 66.05000000001157900, -56.77310748452439526 ) ) ;
#204116=DIRECTION ( 'NONE',  ( 1.000000000000000000, 0.000000000000000000, 0.000000000000000000 ) ) ;
#204148=CARTESIAN_POINT ( 'NONE',  ( 20.73486653747088582, 68.75000000001156764, -60.27310748452437394 ) ) ;
#204164=ORIENTED_EDGE ( 'NONE', *, *, #42890, .T. ) ;
#204344=ADVANCED_FACE ( 'NONE', ( #190471 ), #132357, .T. ) ;
#204412=CARTESIAN_POINT ( 'NONE',  ( -12.42749937872396160, 66.62931007840893471, -51.99664235786332966 ) ) ;
#204434=ORIENTED_EDGE ( 'NONE', *, *, #72833, .F. ) ;
#204505=CARTESIAN_POINT ( 'NONE',  ( -16.93710578446422588, 66.05000000001153637, -48.94191146832373107 ) ) ;
#205062=AXIS2_PLACEMENT_3D ( 'NONE', #165932, #148928, #171092 ) ;
#205453=AXIS2_PLACEMENT_3D ( 'NONE', #80179, #21543, #222263 ) ;
#205644=VERTEX_POINT ( 'NONE', #227340 ) ;
#205701=CARTESIAN_POINT ( 'NONE',  ( -16.94107738177415357, 65.98576071487495653, -56.97310748452440521 ) ) ;
#205793=EDGE_LOOP ( 'NONE', ( #40563, #94949, #162463, #42215, #253334 ) ) ;
#205860=ORIENTED_EDGE ( 'NONE', *, *, #115048, .F. ) ;
#205865=CARTESIAN_POINT ( 'NONE',  ( 20.73486653747088582, 68.75000000001149658, -48.67310748452437963 ) ) ;
#205912=PLANE ( 'NONE',  #201018 ) ;
#206249=CARTESIAN_POINT ( 'NONE',  ( -16.81744102076749314, 66.05000000001157900, -56.87310748452438958 ) ) ;
#206334=ORIENTED_EDGE ( 'NONE', *, *, #176347, .F. ) ;
#206340=ORIENTED_EDGE ( 'NONE', *, *, #226015, .F. ) ;
#206343=VERTEX_POINT ( 'NONE', #144612 ) ;
#206430=CARTESIAN_POINT ( 'NONE',  ( -16.78270389226383230, 66.05262738339450834, -48.68190044761291801 ) ) ;
#206479=VECTOR ( 'NONE', #44558, 1000.000000000000000 ) ;
#206516=AXIS2_PLACEMENT_3D ( 'NONE', #184477, #30577, #187081 ) ;
#206624=VERTEX_POINT ( 'NONE', #24079 ) ;
#206649=CARTESIAN_POINT ( 'NONE',  ( 20.73486653747088937, 68.25000000001156764, -60.27310748452438105 ) ) ;
#206712=CARTESIAN_POINT ( 'NONE',  ( -16.94445028196807002, 66.00793639031378746, -48.63043766294283898 ) ) ;
#207096=CARTESIAN_POINT ( 'NONE',  ( -16.91776028072577631, 66.03659960638177040, -48.64808346982226794 ) ) ;
#207117=EDGE_CURVE ( 'NONE', #94765, #243170, #172296, .T. ) ;
#207135=CARTESIAN_POINT ( 'NONE',  ( -21.64999999999999858, 65.95000000001159890, -56.87310748452438958 ) ) ;
#207364=CARTESIAN_POINT ( 'NONE',  ( -18.40000000000000213, 64.51332499825382172, -45.27310748452440947 ) ) ;
#207378=APPLICATION_CONTEXT ( 'automotive_design' ) ;
#207516=ORIENTED_EDGE ( 'NONE', *, *, #103315, .T. ) ;
#207526=DIRECTION ( 'NONE',  ( -0.000000000000000000, -6.982962677686266711E-15, 1.000000000000000000 ) ) ;
#207566=VECTOR ( 'NONE', #44550, 1000.000000000000000 ) ;
#207610=CARTESIAN_POINT ( 'NONE',  ( -16.89268316805465986, 66.04827818676933759, -48.66735500597884823 ) ) ;
#207736=CARTESIAN_POINT ( 'NONE',  ( -16.79363873026997922, 66.05114977059308501, -48.67695370307892233 ) ) ;
#207846=( BOUNDED_CURVE ( )  B_SPLINE_CURVE ( 3, ( #419, #103366, #182946, #220771 ),
 .UNSPECIFIED., .F., .F. ) 
 B_SPLINE_CURVE_WITH_KNOTS ( ( 4, 4 ),
 ( 5.733388419619901200, 5.983100554402347449 ),
 .UNSPECIFIED. ) 
 CURVE ( )  GEOMETRIC_REPRESENTATION_ITEM ( )  RATIONAL_B_SPLINE_CURVE ( ( 1.000000000000000000, 0.9948104011409417691, 0.9948104011409417691, 1.000000000000000000 ) ) 
 REPRESENTATION_ITEM ( '' )  );
#207891=ORIENTED_EDGE ( 'NONE', *, *, #229824, .F. ) ;
#208288=ORIENTED_EDGE ( 'NONE', *, *, #221990, .T. ) ;
#208294=CARTESIAN_POINT ( 'NONE',  ( -14.22969084473441725, 66.54399267394222761, -51.03447399037762722 ) ) ;
#208576=ORIENTED_EDGE ( 'NONE', *, *, #72860, .F. ) ;
#208612=CARTESIAN_POINT ( 'NONE',  ( -17.22361732159832215, 65.65484434140915937, -58.15232295865727252 ) ) ;
#208794=VERTEX_POINT ( 'NONE', #11736 ) ;
#209103=VERTEX_POINT ( 'NONE', #15274 ) ;
#209393=CARTESIAN_POINT ( 'NONE',  ( -17.11825945287482753, 66.05000000001157900, -56.77310748452439526 ) ) ;
#209654=CARTESIAN_POINT ( 'NONE',  ( -16.86757978335471719, 66.03434962097729510, -56.92510283135688098 ) ) ;
#209773=DIRECTION ( 'NONE',  ( -1.000000000000000000, 7.492892343619937423E-30, -1.073024830501117725E-15 ) ) ;
#209814=ORIENTED_EDGE ( 'NONE', *, *, #15096, .F. ) ;
#209824=LINE ( 'NONE', #49461, #123300 ) ;
#210044=EDGE_LOOP ( 'NONE', ( #41852, #19967, #68754, #149162 ) ) ;
#210060=ORIENTED_EDGE ( 'NONE', *, *, #140570, .F. ) ;
#210419=CARTESIAN_POINT ( 'NONE',  ( -16.89268316805465986, 66.04827818676933759, -48.66735500597884823 ) ) ;
#210938=CARTESIAN_POINT ( 'NONE',  ( -16.93658211146644987, 66.00589133767032024, -48.61881241456871550 ) ) ;
#211038=EDGE_CURVE ( 'NONE', #1286, #245188, #84558, .T. ) ;
#211198=CARTESIAN_POINT ( 'NONE',  ( -18.38204789744325396, 64.52049896284640340, -45.27310748452440947 ) ) ;
#211228=VERTEX_POINT ( 'NONE', #207135 ) ;
#211598=VECTOR ( 'NONE', #155105, 1000.000000000000000 ) ;
#211770=ORIENTED_EDGE ( 'NONE', *, *, #171588, .F. ) ;
#211864=EDGE_CURVE ( 'NONE', #90236, #188280, #236634, .T. ) ;
#212224=CARTESIAN_POINT ( 'NONE',  ( 13.43443725621852991, 66.55344247693902560, -54.43316553017851334 ) ) ;
#212240=CARTESIAN_POINT ( 'NONE',  ( -16.94275863006528482, 66.01050395134400617, -48.63141010244781626 ) ) ;
#212431=VERTEX_POINT ( 'NONE', #161378 ) ;
#212726=CARTESIAN_POINT ( 'NONE',  ( -20.65000000000000568, 70.35000000001153353, -48.67310748452436542 ) ) ;
#212850=CARTESIAN_POINT ( 'NONE',  ( 18.39999999999999503, 67.17743825834509153, -45.27310748452438816 ) ) ;
#212876=FILL_AREA_STYLE ('',( #171224 ) ) ;
#212930=LINE ( 'NONE', #94252, #55152 ) ;
#212992=ORIENTED_EDGE ( 'NONE', *, *, #64401, .F. ) ;
#213004=DIRECTION ( 'NONE',  ( -0.8049926720990042694, 0.5932847527679310229, 4.142885285818786163E-15 ) ) ;
#213104=LINE ( 'NONE', #231403, #61297 ) ;
#213273=CARTESIAN_POINT ( 'NONE',  ( 20.99999999999999645, 66.25000000001159606, -56.87310748452438958 ) ) ;
#213456=LINE ( 'NONE', #132651, #242950 ) ;
#213700=AXIS2_PLACEMENT_3D ( 'NONE', #96255, #173299, #72893 ) ;
#213712=ORIENTED_EDGE ( 'NONE', *, *, #257844, .F. ) ;
#213752=VERTEX_POINT ( 'NONE', #195116 ) ;
#213782=ADVANCED_FACE ( 'NONE', ( #75168 ), #256267, .F. ) ;
#213856=FACE_OUTER_BOUND ( 'NONE', #51149, .T. ) ;
#213994=ORIENTED_EDGE ( 'NONE', *, *, #91271, .F. ) ;
#214271=VERTEX_POINT ( 'NONE', #223314 ) ;
#214278=CARTESIAN_POINT ( 'NONE',  ( 12.30626653967340900, 66.64320997496565724, -52.31828097591050408 ) ) ;
#214297=CARTESIAN_POINT ( 'NONE',  ( 17.74533788810829904, 65.18150020854071158, -46.33673015947196916 ) ) ;
#214323=CARTESIAN_POINT ( 'NONE',  ( -17.22767730083325333, 65.65075578754444052, -47.38067879395489967 ) ) ;
#214610=VECTOR ( 'NONE', #216729, 1000.000000000000000 ) ;
#214711=ORIENTED_EDGE ( 'NONE', *, *, #150607, .F. ) ;
#214752=DIRECTION ( 'NONE',  ( 1.000000000000000000, 0.000000000000000000, 0.000000000000000000 ) ) ;
#214762=CARTESIAN_POINT ( 'NONE',  ( 12.25000000000000000, 66.65000000001155911, -52.77310748452440237 ) ) ;
#214846=ORIENTED_EDGE ( 'NONE', *, *, #95635, .F. ) ;
#215028=B_SPLINE_CURVE_WITH_KNOTS ( 'NONE', 3,
 ( #40733, #44556, #242731, #122816, #103211, #201050, #238902, #4127, #202333, #65390, #22440, #60244, #221867, #100629 ),
 .UNSPECIFIED., .F., .F.,
 ( 4, 2, 2, 2, 2, 2, 4 ),
 ( 0.000000000000000000, 2.389617747642148448E-05, 4.779235495284296897E-05, 9.558470990570041204E-05, 0.0001911694198114009054, 0.0003823388396228294579, 0.0007646776792456864546 ),
 .UNSPECIFIED. ) ;
#215087=CARTESIAN_POINT ( 'NONE',  ( -16.81453563122429529, 66.06089979457456707, -48.73484882387909067 ) ) ;
#215088=ORIENTED_EDGE ( 'NONE', *, *, #86729, .T. ) ;
#215130=CARTESIAN_POINT ( 'NONE',  ( 21.13736287352038445, 67.95335762362759624, -60.27310748452438105 ) ) ;
#215191=DIRECTION ( 'NONE',  ( -3.035766082959430717E-14, -6.982962677686266711E-15, 1.000000000000000000 ) ) ;
#215350=VECTOR ( 'NONE', #185539, 1000.000000000000000 ) ;
#215357=ORIENTED_EDGE ( 'NONE', *, *, #80194, .T. ) ;
#215548=CARTESIAN_POINT ( 'NONE',  ( 15.51872946208854565, 66.62341902196757815, -51.89616123751244459 ) ) ;
#215596=FACE_OUTER_BOUND ( 'NONE', #10201, .T. ) ;
#215845=ORIENTED_EDGE ( 'NONE', *, *, #3424, .F. ) ;
#216120=AXIS2_PLACEMENT_3D ( 'NONE', #2512, #182473, #85883 ) ;
#216336=CARTESIAN_POINT ( 'NONE',  ( 18.54999999999999716, 67.25000000001155342, -56.87310748452438247 ) ) ;
#216729=DIRECTION ( 'NONE',  ( -0.000000000000000000, -6.982962677686266711E-15, 1.000000000000000000 ) ) ;
#216913=ORIENTED_EDGE ( 'NONE', *, *, #198935, .T. ) ;
#217145=ADVANCED_FACE ( 'NONE', ( #223981 ), #14346, .T. ) ;
#217167=CARTESIAN_POINT ( 'NONE',  ( -15.74999999999999645, 66.65000000001154490, -53.00158811269928094 ) ) ;
#217197=CARTESIAN_POINT ( 'NONE',  ( -16.93772744219066340, 66.00645889125922849, -56.92504551255470346 ) ) ;
#217243=FACE_OUTER_BOUND ( 'NONE', #169122, .T. ) ;
#217398=ADVANCED_FACE ( 'NONE', ( #217243 ), #257613, .T. ) ;
#217704=ORIENTED_EDGE ( 'NONE', *, *, #64401, .T. ) ;
#217709=DIRECTION ( 'NONE',  ( -1.000000000000000000, 0.000000000000000000, 0.000000000000000000 ) ) ;
#218033=FACE_OUTER_BOUND ( 'NONE', #76580, .T. ) ;
#218246=CARTESIAN_POINT ( 'NONE',  ( -18.40000000000000213, 64.25000000001153921, -48.67310748452440805 ) ) ;
#218426=DIRECTION ( 'NONE',  ( -0.000000000000000000, -6.982962677686266711E-15, 1.000000000000000000 ) ) ;
#218476=LINE ( 'NONE', #180663, #181193 ) ;
#218617=CARTESIAN_POINT ( 'NONE',  ( -16.87368910959167678, 66.03872618332016486, -56.91061438788380400 ) ) ;
#218773=DIRECTION ( 'NONE',  ( 1.000000000000000000, 0.000000000000000000, 0.000000000000000000 ) ) ;
#218923=CARTESIAN_POINT ( 'NONE',  ( -16.85312964099708211, 66.08639531794378286, -48.92029177809394014 ) ) ;
#219029=ORIENTED_EDGE ( 'NONE', *, *, #92128, .T. ) ;
#219141=B_SPLINE_CURVE_WITH_KNOTS ( 'NONE', 3,
 ( #223978, #186149, #124900, #126155, #27107, #204412, #105287, #106586, #7507, #87020, #73934, #88296, #29673, #72642, #208294, #93450, #169185, #33541, #230409, #13939, #28399, #252523, #248692, #153495, #51743, #113030, #148309, #92175, #229130, #50457 ),
 .UNSPECIFIED., .F., .F.,
 ( 4, 2, 2, 2, 2, 2, 2, 2, 2, 2, 2, 2, 2, 2, 4 ),
 ( 0.000000000000000000, 0.0003422764154113352953, 0.0006845528308226705907, 0.001026829246234005994, 0.001369105661645341181, 0.002053658492468010688, 0.002738211323290680194, 0.003080487738702015164, 0.003422764154113349267, 0.003765040569524684237, 0.004107316984936018774, 0.004449593400347354177, 0.004791869815758687846, 0.005134146231170023250, 0.005476422646581357787 ),
 .UNSPECIFIED. ) ;
#219145=EDGE_CURVE ( 'NONE', #99179, #154587, #57715, .T. ) ;
#219378=ADVANCED_FACE ( 'NONE', ( #70361 ), #192855, .F. ) ;
#219653=CARTESIAN_POINT ( 'NONE',  ( -16.77683809663752257, 66.05000000001153637, -48.67310748452439384 ) ) ;
#219722=CARTESIAN_POINT ( 'NONE',  ( 21.72449340488910252, 65.71604372252048165, -60.27310748452440237 ) ) ;
#219903=CARTESIAN_POINT ( 'NONE',  ( -16.94275863009466576, 66.01050395134919313, -56.91480486656551108 ) ) ;
#220439=ORIENTED_EDGE ( 'NONE', *, *, #25711, .T. ) ;
#220600=DIRECTION ( 'NONE',  ( -0.5932847527679310229, -0.8049926720990042694, -4.984624513800578906E-15 ) ) ;
#220633=CARTESIAN_POINT ( 'NONE',  ( -16.77180007708461673, 66.05000000001157900, -56.88749336556956848 ) ) ;
#220771=CARTESIAN_POINT ( 'NONE',  ( -16.94107738177414291, 65.98576071487489969, -48.57310748452439952 ) ) ;
#221024=CARTESIAN_POINT ( 'NONE',  ( -13.43673303185028800, 66.55335100938270898, -54.43394418860121675 ) ) ;
#221044=LINE ( 'NONE', #204054, #18879 ) ;
#221575=ADVANCED_FACE ( 'NONE', ( #222228 ), #252665, .T. ) ;
#221658=DIRECTION ( 'NONE',  ( 1.000000000000000000, 0.000000000000000000, 0.000000000000000000 ) ) ;
#221867=CARTESIAN_POINT ( 'NONE',  ( -16.87683809663753109, 66.13508622147315918, -56.24739184888585442 ) ) ;
#221990=EDGE_CURVE ( 'NONE', #229182, #202498, #43784, .T. ) ;
#222007=ORIENTED_EDGE ( 'NONE', *, *, #1595, .F. ) ;
#222011=VECTOR ( 'NONE', #121026, 1000.000000000000000 ) ;
#222068=AXIS2_PLACEMENT_3D ( 'NONE', #11668, #35106, #95029 ) ;
#222228=FACE_OUTER_BOUND ( 'NONE', #108048, .T. ) ;
#222245=DIRECTION ( 'NONE',  ( 1.186688945009009831E-16, 1.000000000000000000, 6.982962677686266711E-15 ) ) ;
#222263=DIRECTION ( 'NONE',  ( 0.000000000000000000, 1.000000000000000000, 0.000000000000000000 ) ) ;
#222287=CARTESIAN_POINT ( 'NONE',  ( -12.47155713865592475, 66.62433047358575777, -53.65531747513846739 ) ) ;
#222519=EDGE_CURVE ( 'NONE', #212431, #13073, #50350, .T. ) ;
#222579=ORIENTED_EDGE ( 'NONE', *, *, #187792, .F. ) ;
#222779=CARTESIAN_POINT ( 'NONE',  ( -16.80621392010904813, 66.05779742250376785, -48.71269944994133283 ) ) ;
#222899=CARTESIAN_POINT ( 'NONE',  ( 20.73486653747088582, 68.75000000001155342, -56.87310748452436826 ) ) ;
#222902=DIRECTION ( 'NONE',  ( 0.000000000000000000, 6.982962677686266711E-15, -1.000000000000000000 ) ) ;
#223065=CARTESIAN_POINT ( 'NONE',  ( -23.25000000000000355, 65.95000000001158469, -56.77310748452439526 ) ) ;
#223076=AXIS2_PLACEMENT_3D ( 'NONE', #196345, #116818, #13868 ) ;
#223288=CARTESIAN_POINT ( 'NONE',  ( -23.25000000000000355, 70.35000000001160458, -60.27310748452436684 ) ) ;
#223314=CARTESIAN_POINT ( 'NONE',  ( -18.34374000495059676, 64.52683809664901560, -45.27310748452439526 ) ) ;
#223340=CARTESIAN_POINT ( 'NONE',  ( -16.92570016628983609, 66.04121104227165517, -48.64375815456339325 ) ) ;
#223351=MECHANICAL_DESIGN_GEOMETRIC_PRESENTATION_REPRESENTATION('',(#127516),#194170);
#223478=CARTESIAN_POINT ( 'NONE',  ( -16.97683809663752186, 66.05000000001160743, -60.27310748452439526 ) ) ;
#223904=CARTESIAN_POINT ( 'NONE',  ( -16.84419801905645997, 66.05000000001155058, -48.69259733074643037 ) ) ;
#223957=CARTESIAN_POINT ( 'NONE',  ( 18.54999999999999716, 66.05000000001152216, -48.67310748452433700 ) ) ;
#223978=CARTESIAN_POINT ( 'NONE',  ( -12.25000000000000178, 66.65000000001155911, -52.77310748452439526 ) ) ;
#223981=FACE_OUTER_BOUND ( 'NONE', #145172, .T. ) ;
#224335=EDGE_LOOP ( 'NONE', ( #3088, #124646, #182241, #244736 ) ) ;
#224383=CARTESIAN_POINT ( 'NONE',  ( -16.88560720703333473, 66.04943515626187889, -56.87499556366067566 ) ) ;
#224575=CARTESIAN_POINT ( 'NONE',  ( -16.88328101497759448, 66.04964716579266337, -48.67192796959511725 ) ) ;
#224622=VERTEX_POINT ( 'NONE', #179752 ) ;
#224626=CARTESIAN_POINT ( 'NONE',  ( -16.93388492042257454, 66.01145817749561218, -48.62256236133821830 ) ) ;
#224631=CARTESIAN_POINT ( 'NONE',  ( -16.94107738177414291, 65.98576071487489969, -48.57310748452439952 ) ) ;
#224727=ORIENTED_EDGE ( 'NONE', *, *, #72986, .F. ) ;
#224810=CARTESIAN_POINT ( 'NONE',  ( -16.92570016628985385, 66.04121104227171202, -56.90245681448540438 ) ) ;
#225195=AXIS2_PLACEMENT_3D ( 'NONE', #96121, #152293, #54439 ) ;
#225278=LINE ( 'NONE', #124931, #255840 ) ;
#225418=DIRECTION ( 'NONE',  ( 1.186688945009009831E-16, 1.000000000000000000, 6.982962677686266711E-15 ) ) ;
#225446=ORIENTED_EDGE ( 'NONE', *, *, #128898, .T. ) ;
#225525=DIRECTION ( 'NONE',  ( 1.000000000000000000, 0.000000000000000000, 0.000000000000000000 ) ) ;
#225610=CYLINDRICAL_SURFACE ( 'NONE', #85525, 0.1000000000000028644 ) ;
#225679=CARTESIAN_POINT ( 'NONE',  ( -17.01764560440442864, 66.05000000001159322, -56.77310748530980788 ) ) ;
#225698=EDGE_CURVE ( 'NONE', #19024, #143115, #52118, .T. ) ;
#225747=VECTOR ( 'NONE', #157192, 1000.000000000000000 ) ;
#225954=CARTESIAN_POINT ( 'NONE',  ( 17.74533788810830615, 65.18150020854078264, -59.20948480957681426 ) ) ;
#226015=EDGE_CURVE ( 'NONE', #78170, #156714, #186210, .T. ) ;
#226356=EDGE_CURVE ( 'NONE', #89456, #245959, #24274, .T. ) ;
#226634=CARTESIAN_POINT ( 'NONE',  ( -16.80891096016330266, 66.05000000001153637, -48.65544467725587197 ) ) ;
#226796=AXIS2_PLACEMENT_3D ( 'NONE', #165528, #82094, #44296 ) ;
#226844=ADVANCED_FACE ( 'NONE', ( #82162 ), #198286, .F. ) ;
#226917=ADVANCED_FACE ( 'NONE', ( #231662 ), #83446, .F. ) ;
#227163=CARTESIAN_POINT ( 'NONE',  ( -16.93302609847409457, 66.00331747920836278, -56.93671898916184659 ) ) ;
#227245=LINE ( 'NONE', #128161, #4059 ) ;
#227340=CARTESIAN_POINT ( 'NONE',  ( 20.09999999999999787, 66.25000000001156764, -56.87310748452438958 ) ) ;
#227389=CARTESIAN_POINT ( 'NONE',  ( -16.86420534634261514, 66.02938455441979215, -48.60477093528701431 ) ) ;
#227539=ORIENTED_EDGE ( 'NONE', *, *, #1364, .F. ) ;
#227575=FACE_OUTER_BOUND ( 'NONE', #87400, .T. ) ;
#227910=VECTOR ( 'NONE', #157753, 1000.000000000000000 ) ;
#227987=ADVANCED_FACE ( 'NONE', ( #156971 ), #95674, .T. ) ;
#228050=CARTESIAN_POINT ( 'NONE',  ( -18.34374000495060386, 64.52683809664912928, -60.27310748452440947 ) ) ;
#228130=DIRECTION ( 'NONE',  ( 1.000000000000000000, 0.000000000000000000, 0.000000000000000000 ) ) ;
#228474=CARTESIAN_POINT ( 'NONE',  ( -16.93230518875208190, 65.99924963859173488, -56.94732913642289418 ) ) ;
#228647=DIRECTION ( 'NONE',  ( -1.020425574104004196E-15, -6.982962677686266711E-15, 1.000000000000000000 ) ) ;
#228951=CARTESIAN_POINT ( 'NONE',  ( 21.72449340488910252, 65.71604372252045323, -56.87310748452438958 ) ) ;
#228983=CARTESIAN_POINT ( 'NONE',  ( 18.39999999999999503, 64.25000000001153921, -48.67310748452440805 ) ) ;
#229106=CARTESIAN_POINT ( 'NONE',  ( -21.64999999999999858, 65.95000000001158469, -56.77310748452439526 ) ) ;
#229130=CARTESIAN_POINT ( 'NONE',  ( -15.75000000000001066, 66.65000000001157332, -52.65883987690830992 ) ) ;
#229142=ORIENTED_EDGE ( 'NONE', *, *, #110832, .T. ) ;
#229182=VERTEX_POINT ( 'NONE', #5582 ) ;
#229228=CARTESIAN_POINT ( 'NONE',  ( -16.90987985657661596, 66.04219248183177626, -48.65382039564075001 ) ) ;
#229274=ORIENTED_EDGE ( 'NONE', *, *, #30473, .F. ) ;
#229394=DIRECTION ( 'NONE',  ( 1.000000000000000000, 0.000000000000000000, 0.000000000000000000 ) ) ;
#229422=EDGE_CURVE ( 'NONE', #245188, #128091, #17190, .T. ) ;
#229598=CARTESIAN_POINT ( 'NONE',  ( 23.04999999999999716, 67.17743825834511995, -48.67310748452439384 ) ) ;
#229824=EDGE_CURVE ( 'NONE', #145089, #1286, #254177, .T. ) ;
#230076=VERTEX_POINT ( 'NONE', #183654 ) ;
#230258=CARTESIAN_POINT ( 'NONE',  ( -16.94445028196808778, 66.00793639031384430, -56.91577730610593733 ) ) ;
#230370=ORIENTED_EDGE ( 'NONE', *, *, #74058, .T. ) ;
#230409=CARTESIAN_POINT ( 'NONE',  ( -14.87770893841227249, 66.56936289831479314, -51.25484686646344556 ) ) ;
#230472=EDGE_LOOP ( 'NONE', ( #36740, #194716, #192135, #146930 ) ) ;
#230508=CARTESIAN_POINT ( 'NONE',  ( -16.93301857435210067, 66.02369064527604792, -48.63733191336294226 ) ) ;
#230634=CARTESIAN_POINT ( 'NONE',  ( -18.39999999999999858, 64.52132590001231449, -60.24841426818374401 ) ) ;
#230928=CIRCLE ( 'NONE', #226796, 1.749999999999998002 ) ;
#231000=DIRECTION ( 'NONE',  ( -1.000000000000000000, 0.000000000000000000, 0.000000000000000000 ) ) ;
#231174=SURFACE_STYLE_USAGE ( .BOTH. , #34265 ) ;
#231364=DIRECTION ( 'NONE',  ( -1.000000000000000000, 0.000000000000000000, 0.000000000000000000 ) ) ;
#231403=CARTESIAN_POINT ( 'NONE',  ( 21.72449340488910252, 65.71604372252045323, -56.87310748452438958 ) ) ;
#231473=CARTESIAN_POINT ( 'NONE',  ( -16.77828822508139694, 66.05377062509082009, -56.86047923315044272 ) ) ;
#231662=FACE_OUTER_BOUND ( 'NONE', #22980, .T. ) ;
#231781=CARTESIAN_POINT ( 'NONE',  ( 13.54556439290364089, 66.54940788787787653, -54.46691916571600700 ) ) ;
#231800=CARTESIAN_POINT ( 'NONE',  ( -16.87036670365549895, 66.01058118070993430, -57.00266760182645243 ) ) ;
#231986=DIRECTION ( 'NONE',  ( -1.000000000000000000, 0.000000000000000000, -0.000000000000000000 ) ) ;
#232085=DIRECTION ( 'NONE',  ( 0.000000000000000000, 1.000000000000000000, 6.982962677686266711E-15 ) ) ;
#232151=CARTESIAN_POINT ( 'NONE',  ( -16.86132326855786800, 66.05000000001156479, -56.82447169985605484 ) ) ;
#232328=ORIENTED_EDGE ( 'NONE', *, *, #157557, .T. ) ;
#232332=CARTESIAN_POINT ( 'NONE',  ( -16.93262454970420094, 65.99797953208121726, -56.95018371076170638 ) ) ;
#232651=DIRECTION ( 'NONE',  ( 0.000000000000000000, 1.000000000000000000, 6.982962677686266711E-15 ) ) ;
#232964=ORIENTED_EDGE ( 'NONE', *, *, #242859, .T. ) ;
#233444=DIRECTION ( 'NONE',  ( 1.000000000000000000, 0.000000000000000000, 0.000000000000000000 ) ) ;
#233655=ADVANCED_FACE ( 'NONE', ( #128878 ), #126286, .F. ) ;
#233840=CARTESIAN_POINT ( 'NONE',  ( 15.69410316191959254, 66.64325398293328817, -52.31974776316020126 ) ) ;
#233842=DIRECTION ( 'NONE',  ( 0.000000000000000000, -1.000000000000000000, -6.982962677686266711E-15 ) ) ;
#234198=DIRECTION ( 'NONE',  ( 1.000000000000000000, 0.000000000000000000, 0.000000000000000000 ) ) ;
#234337=CARTESIAN_POINT ( 'NONE',  ( -16.93826681692523550, 65.98857127972381420, -48.57764901716495842 ) ) ;
#234631=CARTESIAN_POINT ( 'NONE',  ( -18.34374000495059676, 64.52683809664901560, -45.27310748452439526 ) ) ;
#234693=ORIENTED_EDGE ( 'NONE', *, *, #188434, .T. ) ;
#234755=EDGE_CURVE ( 'NONE', #243170, #13299, #118035, .T. ) ;
#234868=EDGE_CURVE ( 'NONE', #48902, #190074, #46687, .T. ) ;
#234871=ORIENTED_EDGE ( 'NONE', *, *, #187792, .T. ) ;
#235397=CARTESIAN_POINT ( 'NONE',  ( -18.40000000000000213, 70.35000000001153353, -48.67310748452436542 ) ) ;
#235427=DIRECTION ( 'NONE',  ( -1.000000000000000000, 0.000000000000000000, 0.000000000000000000 ) ) ;
#235449=VERTEX_POINT ( 'NONE', #129294 ) ;
#235518=CARTESIAN_POINT ( 'NONE',  ( -17.11825945287481687, 65.95000000001152785, -48.67310748452439384 ) ) ;
#235537=EDGE_LOOP ( 'NONE', ( #52672, #28261, #197495, #210060 ) ) ;
#235604=CARTESIAN_POINT ( 'NONE',  ( -16.94389599338512298, 66.00880201025651672, -56.91546268271414988 ) ) ;
#235618=CARTESIAN_POINT ( 'NONE',  ( -16.93294127766158752, 65.99671989705664998, -48.59320021869516637 ) ) ;
#235620=CARTESIAN_POINT ( 'NONE',  ( -16.87845715379269507, 66.04214188611454972, -56.89930683346550211 ) ) ;
#235626=FACE_OUTER_BOUND ( 'NONE', #39280, .T. ) ;
#235924=CARTESIAN_POINT ( 'NONE',  ( -16.78493211734303259, 66.05416425680736836, -48.68705650362843329 ) ) ;
#236098=ORIENTED_EDGE ( 'NONE', *, *, #89942, .F. ) ;
#236259=CYLINDRICAL_SURFACE ( 'NONE', #154173, 0.1000000000000050432 ) ;
#236319=AXIS2_PLACEMENT_3D ( 'NONE', #35253, #194323, #233444 ) ;
#236432=DIRECTION ( 'NONE',  ( -1.073024830501117725E-15, -6.982962677686266711E-15, 1.000000000000000000 ) ) ;
#236634=LINE ( 'NONE', #257431, #19362 ) ;
#236735=CARTESIAN_POINT ( 'NONE',  ( -15.75000000000000355, 66.65000000001155911, -52.77310748452439526 ) ) ;
#236767=CARTESIAN_POINT ( 'NONE',  ( -16.94445028196808778, 66.00793639031384430, -56.91577730610593733 ) ) ;
#236769=B_SPLINE_CURVE_WITH_KNOTS ( 'NONE', 3,
 ( #33897, #249061, #247756, #211198, #32606, #69144, #207364 ),
 .UNSPECIFIED., .F., .F.,
 ( 4, 3, 4 ),
 ( 3.469446951953614189E-18, 3.882884552234413058E-05, 5.798605692158429121E-05 ),
 .UNSPECIFIED. ) ;
#236897=CARTESIAN_POINT ( 'NONE',  ( -16.94445028196808778, 66.00793639031384430, -56.91577730610593733 ) ) ;
#236954=ORIENTED_EDGE ( 'NONE', *, *, #250280, .F. ) ;
#237232=CARTESIAN_POINT ( 'NONE',  ( -16.87683809663752399, 66.15000000001153069, -49.42547150272071121 ) ) ;
#237474=ORIENTED_EDGE ( 'NONE', *, *, #91271, .T. ) ;
#237496=ORIENTED_EDGE ( 'NONE', *, *, #138512, .F. ) ;
#237599=CARTESIAN_POINT ( 'NONE',  ( -16.87683809663752399, 66.15000000001158753, -56.87310748452438958 ) ) ;
#237619=CARTESIAN_POINT ( 'NONE',  ( -21.65000000000000213, 68.75000000001153921, -48.67310748452437252 ) ) ;
#237631=CARTESIAN_POINT ( 'NONE',  ( -16.97683810757273193, 66.05000000001157900, -56.25953077206424524 ) ) ;
#237690=CARTESIAN_POINT ( 'NONE',  ( 12.25000000000000000, 66.65000000001155911, -52.65883987690830281 ) ) ;
#238026=CARTESIAN_POINT ( 'NONE',  ( -12.25000000000000178, 66.65000000001155911, -52.77310748452439526 ) ) ;
#238101=CARTESIAN_POINT ( 'NONE',  ( 23.04999999999999716, 67.17743825834520521, -60.27310748452438816 ) ) ;
#238182=CARTESIAN_POINT ( 'NONE',  ( -16.94445028196807002, 66.00793639031378746, -48.63043766294283898 ) ) ;
#238581=CARTESIAN_POINT ( 'NONE',  ( -18.40000000000000213, 64.58541674041178737, -56.87310748452438958 ) ) ;
#238643=AXIS2_PLACEMENT_3D ( 'NONE', #132147, #31800, #192146 ) ;
#238902=CARTESIAN_POINT ( 'NONE',  ( -16.81930730667006557, 66.06300193113754915, -56.79633975398618873 ) ) ;
#239052=LINE ( 'NONE', #421, #97998 ) ;
#239069=ORIENTED_EDGE ( 'NONE', *, *, #211038, .F. ) ;
#239092=LINE ( 'NONE', #82542, #66001 ) ;
#239112=VERTEX_POINT ( 'NONE', #205865 ) ;
#239303=CYLINDRICAL_SURFACE ( 'NONE', #91346, 0.9000000000000014655 ) ;
#239325=CARTESIAN_POINT ( 'NONE',  ( -14.56556274378147720, 66.55344247693902560, -54.43316553017852044 ) ) ;
#239421=VECTOR ( 'NONE', #231000, 1000.000000000000000 ) ;
#239665=UNCERTAINTY_MEASURE_WITH_UNIT (LENGTH_MEASURE( 1.000000000000000082E-05 ), #198158, 'distance_accuracy_value', 'NONE');
#239893=DIRECTION ( 'NONE',  ( 0.000000000000000000, -1.000000000000000000, -6.982962677686266711E-15 ) ) ;
#239930=EDGE_LOOP ( 'NONE', ( #28979, #11023, #92725, #156676, #95273, #65295, #105301, #141746, #76479, #249514, #100744, #32122, #59024, #54405, #170365, #141535, #150843, #22264 ) ) ;
#240116=CARTESIAN_POINT ( 'NONE',  ( -16.89268316805466341, 66.04827818676939444, -56.87885996306994230 ) ) ;
#240205=CARTESIAN_POINT ( 'NONE',  ( -16.83233564386412340, 66.06977820342686414, -56.74762814800010347 ) ) ;
#240254=ORIENTED_EDGE ( 'NONE', *, *, #159489, .F. ) ;
#240604=CARTESIAN_POINT ( 'NONE',  ( -14.77738660682463845, 66.56344716000714357, -54.34515201176409249 ) ) ;
#240766=CARTESIAN_POINT ( 'NONE',  ( 16.27683809663750125, 66.65000000001161595, -60.27310748452439526 ) ) ;
#240792=LINE ( 'NONE', #26906, #91703 ) ;
#240935=ORIENTED_EDGE ( 'NONE', *, *, #122078, .T. ) ;
#240945=LINE ( 'NONE', #180975, #222011 ) ;
#240997=CARTESIAN_POINT ( 'NONE',  ( -17.78241384941187420, 65.14442424719499058, -59.27406981206009817 ) ) ;
#241051=VECTOR ( 'NONE', #49453, 1000.000000000000000 ) ;
#241094=VERTEX_POINT ( 'NONE', #5785 ) ;
#241101=CARTESIAN_POINT ( 'NONE',  ( -16.79270642812312531, 66.05375578307346984, -48.68417420596193779 ) ) ;
#241258=CARTESIAN_POINT ( 'NONE',  ( 18.39999999999999503, 64.25000000001151079, -45.27310748452440237 ) ) ;
#241499=EDGE_CURVE ( 'NONE', #213752, #16468, #188964, .T. ) ;
#241583=CARTESIAN_POINT ( 'NONE',  ( -18.44085059012131822, 64.48598750652770661, -45.28280216540286318 ) ) ;
#241814=CARTESIAN_POINT ( 'NONE',  ( -16.91256925476571737, 66.01426884188337851, -56.99074997352966676 ) ) ;
#241951=CARTESIAN_POINT ( 'NONE',  ( -16.77683809663752257, 52.34166666667822199, -52.77310748452448763 ) ) ;
#242044=EDGE_LOOP ( 'NONE', ( #48473, #74014, #70812, #94413, #20747, #136035, #30702, #207891, #256702 ) ) ;
#242181=LINE ( 'NONE', #161385, #164743 ) ;
#242259=CARTESIAN_POINT ( 'NONE',  ( -18.37013991200266005, 64.50025238379961934, -60.31613049504152002 ) ) ;
#242411=( NAMED_UNIT ( * ) SI_UNIT ( $, .STERADIAN. ) SOLID_ANGLE_UNIT ( ) );
#242731=CARTESIAN_POINT ( 'NONE',  ( -16.79139129368504513, 66.05505583754988663, -56.85286285169858189 ) ) ;
#242779=EDGE_LOOP ( 'NONE', ( #9136, #81885, #5444 ) ) ;
#242859=EDGE_CURVE ( 'NONE', #98576, #245959, #48287, .T. ) ;
#242910=CARTESIAN_POINT ( 'NONE',  ( -16.87242674293849376, 66.05000000001153637, -48.67201723815204417 ) ) ;
#242935=DIRECTION ( 'NONE',  ( 0.000000000000000000, -1.000000000000000000, -6.837150591533219968E-15 ) ) ;
#242950=VECTOR ( 'NONE', #34856, 1000.000000000000000 ) ;
#243040=CARTESIAN_POINT ( 'NONE',  ( 18.39999999999999503, 64.25000000001159606, -56.87310748452440379 ) ) ;
#243085=EDGE_LOOP ( 'NONE', ( #135628, #229142, #239069, #215357 ) ) ;
#243098=CARTESIAN_POINT ( 'NONE',  ( -16.94107738177415712, 65.98576071487495653, -56.97310748452439810 ) ) ;
#243170=VERTEX_POINT ( 'NONE', #107756 ) ;
#243342=ORIENTED_EDGE ( 'NONE', *, *, #198935, .F. ) ;
#243509=CARTESIAN_POINT ( 'NONE',  ( 20.27550659511089037, 66.78395627750272467, -56.87310748452438247 ) ) ;
#243552=CARTESIAN_POINT ( 'NONE',  ( -17.80356949363740782, 65.12326860301170939, -59.23618050875686691 ) ) ;
#243577=VERTEX_POINT ( 'NONE', #61291 ) ;
#243785=ORIENTED_EDGE ( 'NONE', *, *, #198967, .T. ) ;
#243846=EDGE_CURVE ( 'NONE', #211228, #139671, #49426, .T. ) ;
#243865=ORIENTED_EDGE ( 'NONE', *, *, #30710, .T. ) ;
#243924=EDGE_LOOP ( 'NONE', ( #122984, #66258, #249877, #127097 ) ) ;
#243951=CARTESIAN_POINT ( 'NONE',  ( -16.87435696428308063, 66.04999753707934929, -56.87311571935783405 ) ) ;
#244133=CARTESIAN_POINT ( 'NONE',  ( -16.89208623190940273, 66.04842205103602737, -48.66783528130612524 ) ) ;
#244204=CARTESIAN_POINT ( 'NONE',  ( -23.25000000000000355, 70.35000000001153353, -48.67310748452436542 ) ) ;
#244268=VECTOR ( 'NONE', #251172, 1000.000000000000000 ) ;
#244674=CARTESIAN_POINT ( 'NONE',  ( -18.40000000000000213, 64.52683809664901560, -45.34905355133235361 ) ) ;
#244736=ORIENTED_EDGE ( 'NONE', *, *, #180357, .F. ) ;
#244813=EDGE_LOOP ( 'NONE', ( #135097, #116208, #193950, #110474, #174011 ) ) ;
#244829=CARTESIAN_POINT ( 'NONE',  ( -16.87036670365549540, 66.01058118070992009, -57.00266760182645953 ) ) ;
#244924=CARTESIAN_POINT ( 'NONE',  ( -16.96982749440705973, 66.05000000001153637, -49.14788589333611668 ) ) ;
#244965=CARTESIAN_POINT ( 'NONE',  ( -18.40000000000000213, 70.35000000001159037, -56.87310748452436115 ) ) ;
#245132=AXIS2_PLACEMENT_3D ( 'NONE', #36030, #154708, #234198 ) ;
#245188=VERTEX_POINT ( 'NONE', #212726 ) ;
#245450=CARTESIAN_POINT ( 'NONE',  ( -16.89146115310546037, 66.04855675435506157, -48.66828506557018130 ) ) ;
#245488=EDGE_LOOP ( 'NONE', ( #100866, #83570, #38439, #156179, #18382, #79314, #167934, #150894, #172358, #7680, #62715, #212992, #185769, #108288 ) ) ;
#245613=ORIENTED_EDGE ( 'NONE', *, *, #234755, .T. ) ;
#245676=CARTESIAN_POINT ( 'NONE',  ( -16.92778301347306424, 65.99905508317604585, -56.95162559249263268 ) ) ;
#245806=ORIENTED_EDGE ( 'NONE', *, *, #10009, .T. ) ;
#245812=APPLICATION_CONTEXT ( 'automotive_design' ) ;
#245959=VERTEX_POINT ( 'NONE', #96431 ) ;
#246218=CARTESIAN_POINT ( 'NONE',  ( -16.87401514999239893, 66.05000000001153637, -48.74308949199231478 ) ) ;
#246266=ORIENTED_EDGE ( 'NONE', *, *, #102781, .F. ) ;
#246533=CARTESIAN_POINT ( 'NONE',  ( -16.87331047859649757, 66.05000000001153637, -48.67310748452439384 ) ) ;
#246576=EDGE_CURVE ( 'NONE', #45783, #78170, #240792, .T. ) ;
#246708=CARTESIAN_POINT ( 'NONE',  ( -16.87665923198281348, 66.05000000001153637, -48.67310748452439384 ) ) ;
#246722=CARTESIAN_POINT ( 'NONE',  ( -16.93970660449832621, 65.98715860837600644, -56.97082574872992922 ) ) ;
#247105=ORIENTED_EDGE ( 'NONE', *, *, #76576, .T. ) ;
#247330=CARTESIAN_POINT ( 'NONE',  ( -16.89021194854739605, 66.05000000001153637, -48.78053935292005150 ) ) ;
#247455=CARTESIAN_POINT ( 'NONE',  ( -18.40000000000000213, 64.25000000001151079, -45.27310748452440237 ) ) ;
#247605=CARTESIAN_POINT ( 'NONE',  ( -18.37160782347004329, 64.52438358520920758, -60.27310748452440947 ) ) ;
#247756=CARTESIAN_POINT ( 'NONE',  ( -18.36973785203555920, 64.52449679952728445, -45.27310748452440947 ) ) ;
#247848=CARTESIAN_POINT ( 'NONE',  ( -16.95709691156365650, 66.05000000001160743, -56.86304992201380060 ) ) ;
#248110=DIRECTION ( 'NONE',  ( -0.000000000000000000, -6.982962677686266711E-15, 1.000000000000000000 ) ) ;
#248269=VECTOR ( 'NONE', #56317, 1000.000000000000000 ) ;
#248623=VECTOR ( 'NONE', #159357, 1000.000000000000000 ) ;
#248692=CARTESIAN_POINT ( 'NONE',  ( -15.39126916658603683, 66.61042836546512547, -51.70546677215521925 ) ) ;
#248852=FACE_OUTER_BOUND ( 'NONE', #243085, .T. ) ;
#249024=CARTESIAN_POINT ( 'NONE',  ( -16.87036670365549895, 66.01058118070993430, -57.00266760182645243 ) ) ;
#249061=CARTESIAN_POINT ( 'NONE',  ( -18.35668295345803713, 64.52683809664902981, -45.27310748452439526 ) ) ;
#249152=CARTESIAN_POINT ( 'NONE',  ( -17.05016517656107311, 66.05000000001159322, -56.85040948852552845 ) ) ;
#249506=VERTEX_POINT ( 'NONE', #114126 ) ;
#249514=ORIENTED_EDGE ( 'NONE', *, *, #110871, .T. ) ;
#249543=CARTESIAN_POINT ( 'NONE',  ( -16.86337532320260735, 66.02003279578715933, -48.57418301554158546 ) ) ;
#249558=CARTESIAN_POINT ( 'NONE',  ( -18.40000000000000568, 64.52683809664904402, -48.63168612828709314 ) ) ;
#249568=AXIS2_PLACEMENT_3D ( 'NONE', #219722, #200179, #176774 ) ;
#249581=CARTESIAN_POINT ( 'NONE',  ( 17.23472005113826810, 65.69211804551073897, -47.47653062445572658 ) ) ;
#249877=ORIENTED_EDGE ( 'NONE', *, *, #54820, .F. ) ;
#250048=CARTESIAN_POINT ( 'NONE',  ( 13.76927104934457802, 66.54401276639883633, -54.51157631762657729 ) ) ;
#250280=EDGE_CURVE ( 'NONE', #105113, #100756, #96844, .T. ) ;
#250401=CARTESIAN_POINT ( 'NONE',  ( -18.39999999999999858, 64.25000000001161027, -60.27310748452440947 ) ) ;
#250554=ORIENTED_EDGE ( 'NONE', *, *, #75590, .F. ) ;
#250834=DIRECTION ( 'NONE',  ( 0.5932847527679310229, 0.8049926720990042694, 5.621233785078285907E-15 ) ) ;
#250890=ORIENTED_EDGE ( 'NONE', *, *, #167520, .F. ) ;
#250894=VERTEX_POINT ( 'NONE', #145597 ) ;
#251070=ORIENTED_EDGE ( 'NONE', *, *, #25711, .F. ) ;
#251172=DIRECTION ( 'NONE',  ( 0.000000000000000000, -1.000000000000000000, -6.982962677686266711E-15 ) ) ;
#251316=CARTESIAN_POINT ( 'NONE',  ( 15.15590539855246277, 66.58931770574362474, -54.09196404257614432 ) ) ;
#251528=AXIS2_PLACEMENT_3D ( 'NONE', #103024, #225525, #26087 ) ;
#251743=ORIENTED_EDGE ( 'NONE', *, *, #192345, .T. ) ;
#251859=CARTESIAN_POINT ( 'NONE',  ( -16.93583594267724379, 65.99137656495938131, -56.96371664520363964 ) ) ;
#252033=DIRECTION ( 'NONE',  ( -1.000000000000000000, 0.000000000000000000, -0.000000000000000000 ) ) ;
#252102=CARTESIAN_POINT ( 'NONE',  ( -18.40000000000000213, 64.52683809664902981, -48.57310748452440663 ) ) ;
#252149=CARTESIAN_POINT ( 'NONE',  ( -16.87036670365548474, 66.01058118070986325, -48.54354736722234520 ) ) ;
#252266=CARTESIAN_POINT ( 'NONE',  ( -21.64999999999999858, 66.65000000001153069, -48.67310748452439384 ) ) ;
#252284=CARTESIAN_POINT ( 'NONE',  ( -16.77779411503079032, 66.05389855308744984, -56.86005006690456298 ) ) ;
#252459=VECTOR ( 'NONE', #167525, 1000.000000000000000 ) ;
#252523=CARTESIAN_POINT ( 'NONE',  ( -15.31895204843005054, 66.60346600605763001, -51.61716770535109333 ) ) ;
#252576=EDGE_CURVE ( 'NONE', #180347, #99076, #139746, .T. ) ;
#252600=CARTESIAN_POINT ( 'NONE',  ( 15.52844286134407881, 66.62433047358577198, -53.65531747513846739 ) ) ;
#252665=( BOUNDED_SURFACE ( )  B_SPLINE_SURFACE ( 3, 2, ( 
 ( #243098, #241814, #81427 ),
 ( #245676, #7053, #64476 ),
 ( #161007, #67039, #61902 ),
 ( #123164, #224810, #141429 ) ),
 .UNSPECIFIED., .F., .F., .F. ) 
 B_SPLINE_SURFACE_WITH_KNOTS ( ( 4, 4 ),
 ( 3, 3 ),
 ( 0.0008258556059633759532, 0.0009616864997632785118 ),
 ( 0.000000000000000000, 1.000000000000000000 ),
 .UNSPECIFIED. ) 
 GEOMETRIC_REPRESENTATION_ITEM ( )  RATIONAL_B_SPLINE_SURFACE ( (
 ( 1.000000000000000000, 0.9152888060719408525, 1.000000000000000000),
 ( 1.000000000000000000, 0.9327727094138127395, 1.000000000000000000),
 ( 1.000000000000000000, 0.9369023509258341820, 1.000000000000000000),
 ( 1.000000000000000000, 0.9246339933864554661, 1.000000000000000000) ) ) 
 REPRESENTATION_ITEM ( '' )  SURFACE ( )  );
#252800=CARTESIAN_POINT ( 'NONE',  ( -18.40000000000000213, 70.35000000001153353, -48.67310748452436542 ) ) ;
#252986=PRODUCT_CONTEXT ( 'NONE', #207378, 'mechanical' ) ;
#253073=EDGE_CURVE ( 'NONE', #12212, #211228, #119184, .T. ) ;
#253179=ORIENTED_EDGE ( 'NONE', *, *, #198049, .T. ) ;
#253334=ORIENTED_EDGE ( 'NONE', *, *, #171588, .T. ) ;
#253529=CARTESIAN_POINT ( 'NONE',  ( 21.72449340488910607, 65.71604372252041060, -48.67310748452440095 ) ) ;
#253605=CIRCLE ( 'NONE', #170469, 0.1000000000000028644 ) ;
#253650=LINE ( 'NONE', #75063, #135528 ) ;
#253722=ADVANCED_FACE ( 'NONE', ( #186815 ), #65032, .T. ) ;
#253814=VERTEX_POINT ( 'NONE', #189376 ) ;
#253916=ORIENTED_EDGE ( 'NONE', *, *, #123615, .T. ) ;
#254044=AXIS2_PLACEMENT_3D ( 'NONE', #123823, #85935, #164238 ) ;
#254177=LINE ( 'NONE', #118559, #257223 ) ;
#254187=CARTESIAN_POINT ( 'NONE',  ( 20.27550659511089037, 66.78395627750266783, -48.67310748452439384 ) ) ;
#254195=CARTESIAN_POINT ( 'NONE',  ( -16.83794479845802172, 66.07364258066000673, -48.82666278030208673 ) ) ;
#254408=DIRECTION ( 'NONE',  ( 1.000000000000000000, 0.000000000000000000, 0.000000000000000000 ) ) ;
#254423=VERTEX_POINT ( 'NONE', #140286 ) ;
#254647=CARTESIAN_POINT ( 'NONE',  ( 12.25000000000000000, 66.65000000001155911, -52.77310748452440237 ) ) ;
#254660=DIRECTION ( 'NONE',  ( -0.7071067811865463515, 0.7071067811865487940, 4.178957128135655137E-15 ) ) ;
#255103=ORIENTED_EDGE ( 'NONE', *, *, #75590, .T. ) ;
#255123=CARTESIAN_POINT ( 'NONE',  ( 12.47034474403012183, 66.62446189796352769, -53.65323160353356968 ) ) ;
#255782=CARTESIAN_POINT ( 'NONE',  ( -16.27683809663750480, 66.65000000001161595, -60.27310748452439526 ) ) ;
#255840=VECTOR ( 'NONE', #188740, 1000.000000000000000 ) ;
#255864=ADVANCED_FACE ( 'NONE', ( #179520 ), #62127, .F. ) ;
#256128=CARTESIAN_POINT ( 'NONE',  ( -23.25000000000000355, 64.25000000001153921, -48.67310748452440805 ) ) ;
#256267=CYLINDRICAL_SURFACE ( 'NONE', #245132, 1.749999999999999778 ) ;
#256341=EDGE_CURVE ( 'NONE', #99076, #19990, #55463, .T. ) ;
#256597=DIRECTION ( 'NONE',  ( 1.073024830501117725E-15, 6.982962677686266711E-15, -1.000000000000000000 ) ) ;
#256608=VERTEX_POINT ( 'NONE', #148610 ) ;
#256650=ORIENTED_EDGE ( 'NONE', *, *, #234868, .F. ) ;
#256673=ORIENTED_EDGE ( 'NONE', *, *, #164993, .T. ) ;
#256702=ORIENTED_EDGE ( 'NONE', *, *, #107805, .F. ) ;
#256784=ORIENTED_EDGE ( 'NONE', *, *, #56548, .F. ) ;
#256819=CARTESIAN_POINT ( 'NONE',  ( -18.40000000000000213, 64.25000000001151079, -45.27310748452440947 ) ) ;
#257015=DIRECTION ( 'NONE',  ( 0.000000000000000000, -1.000000000000000000, -6.982962677686266711E-15 ) ) ;
#257056=CARTESIAN_POINT ( 'NONE',  ( -15.55912972643740488, 67.50912972644894694, -48.57310748452438531 ) ) ;
#257195=CARTESIAN_POINT ( 'NONE',  ( 12.84435279558019438, 66.58929125296442919, -51.45389907868029411 ) ) ;
#257223=VECTOR ( 'NONE', #232085, 1000.000000000000000 ) ;
#257285=EDGE_LOOP ( 'NONE', ( #36828, #115125, #31304, #12593 ) ) ;
#257431=CARTESIAN_POINT ( 'NONE',  ( 20.73486653747088226, 68.75000000001155342, -56.87310748452436826 ) ) ;
#257535=CARTESIAN_POINT ( 'NONE',  ( -12.60206096961792355, 66.61031399435590572, -53.85026397817309629 ) ) ;
#257613=PLANE ( 'NONE',  #135051 ) ;
#257672=EDGE_LOOP ( 'NONE', ( #194655, #178091, #164964, #22394 ) ) ;
#257706=DIRECTION ( 'NONE',  ( 0.000000000000000000, 6.982962677686266711E-15, -1.000000000000000000 ) ) ;
#257769=( GEOMETRIC_REPRESENTATION_CONTEXT ( 3 ) GLOBAL_UNCERTAINTY_ASSIGNED_CONTEXT ( ( #239665 ) ) GLOBAL_UNIT_ASSIGNED_CONTEXT ( ( #198158, #6373, #242411 ) ) REPRESENTATION_CONTEXT ( 'NONE', 'WORKASPACE' ) );
#257844=EDGE_CURVE ( 'NONE', #188280, #22343, #196738, .T. ) ;
#257883=CARTESIAN_POINT ( 'NONE',  ( 20.99999999999999645, 66.25000000001159606, -56.87310748452438958 ) ) ;
#258031=CARTESIAN_POINT ( 'NONE',  ( -16.81744102076748959, 66.05000000001153637, -48.67310748452439384 ) ) ;
ENDSEC;
END-ISO-10303-21;
